ISO-10303-21;
HEADER;
FILE_DESCRIPTION (('STEP AP214'),
    '1' );
FILE_NAME ('722909.step',
    '2026-11-01T06:29:40',
    ( '' ),
    ( '' ),
    'SwSTEP 2.0',
    'SolidWorks 2024',
    '' );
FILE_SCHEMA (( 'AUTOMOTIVE_DESIGN' ));
ENDSEC;

DATA;
#4=VECTOR ( 'NONE', #1061, 1000.000000000000227 ) ;
#57=DIRECTION ( 'NONE',  ( -1.000000000000000000, 0.000000000000000000, 0.000000000000000000 ) ) ;
#58=ADVANCED_FACE ( 'NONE', ( #14835 ), #17880, .T. ) ;
#68=EDGE_CURVE ( 'NONE', #13953, #12573, #6706, .T. ) ;
#101=CARTESIAN_POINT ( 'NONE',  ( 4.025000000000000355, 0.000000000000000000, 0.000000000000000000 ) ) ;
#117=ORIENTED_EDGE ( 'NONE', *, *, #15149, .T. ) ;
#187=EDGE_CURVE ( 'NONE', #8093, #1892, #19205, .T. ) ;
#203=VECTOR ( 'NONE', #508, 1000.000000000000114 ) ;
#205=DIRECTION ( 'NONE',  ( 1.000000000000000000, 0.000000000000000000, 0.000000000000000000 ) ) ;
#247=DIRECTION ( 'NONE',  ( 1.000000000000000000, 0.000000000000000000, 0.000000000000000000 ) ) ;
#269=ORIENTED_EDGE ( 'NONE', *, *, #15161, .F. ) ;
#282=CARTESIAN_POINT ( 'NONE',  ( 7.000000000000000000, 17.85000000000000142, 0.000000000000000000 ) ) ;
#289=ORIENTED_EDGE ( 'NONE', *, *, #3879, .T. ) ;
#295=CONICAL_SURFACE ( 'NONE', #19035, 13.89560290347679938, 1.567266246505109928 ) ;
#296=VERTEX_POINT ( 'NONE', #2879 ) ;
#299=CARTESIAN_POINT ( 'NONE',  ( 5.425003271131650706, 0.000000000000000000, 0.000000000000000000 ) ) ;
#321=ORIENTED_EDGE ( 'NONE', *, *, #5960, .T. ) ;
#333=ORIENTED_EDGE ( 'NONE', *, *, #2827, .F. ) ;
#409=CARTESIAN_POINT ( 'NONE',  ( 5.941205806953520074, 1.854262922671694143E-15, 15.14120580695351670 ) ) ;
#415=CARTESIAN_POINT ( 'NONE',  ( 1.050000000000000044, 15.25000000000000000, 0.000000000000000000 ) ) ;
#482=EDGE_LOOP ( 'NONE', ( #11298, #10691 ) ) ;
#487=CARTESIAN_POINT ( 'NONE',  ( 0.6999999999999999556, 0.000000000000000000, 0.000000000000000000 ) ) ;
#488=VECTOR ( 'NONE', #2515, 1000.000000000000000 ) ;
#508=DIRECTION ( 'NONE',  ( -0.9740972002433518906, -0.2261297071993489949, -2.769290221138109488E-17 ) ) ;
#518=CARTESIAN_POINT ( 'NONE',  ( 5.941205806953520074, -15.14120580695428764, -1.854262922671788806E-15 ) ) ;
#529=CARTESIAN_POINT ( 'NONE',  ( 5.941205806953520074, 0.000000000000000000, 0.000000000000000000 ) ) ;
#546=DIRECTION ( 'NONE',  ( 0.000000000000000000, 1.000000000000000000, 0.000000000000000000 ) ) ;
#570=CARTESIAN_POINT ( 'NONE',  ( 7.000000000000000000, -17.85000000000000142, -2.225795557450314789E-15 ) ) ;
#603=AXIS2_PLACEMENT_3D ( 'NONE', #20232, #17541, #4790 ) ;
#650=CARTESIAN_POINT ( 'NONE',  ( 7.000000000000000000, 0.000000000000000000, 0.000000000000000000 ) ) ;
#680=EDGE_CURVE ( 'NONE', #13953, #18077, #20051, .T. ) ;
#682=DIRECTION ( 'NONE',  ( 0.000000000000000000, 1.000000000000000000, 0.000000000000000000 ) ) ;
#702=CARTESIAN_POINT ( 'NONE',  ( 4.899999999999999467, 0.000000000000000000, 0.000000000000000000 ) ) ;
#705=ADVANCED_FACE ( 'NONE', ( #1184 ), #8050, .T. ) ;
#706=DIRECTION ( 'NONE',  ( 0.000000000000000000, 1.000000000000000000, 0.000000000000000000 ) ) ;
#718=DIRECTION ( 'NONE',  ( 0.000000000000000000, 1.000000000000000000, 0.000000000000000000 ) ) ;
#719=VECTOR ( 'NONE', #11315, 1000.000000000000000 ) ;
#765=AXIS2_PLACEMENT_3D ( 'NONE', #12536, #17276, #3164 ) ;
#807=CARTESIAN_POINT ( 'NONE',  ( 4.549999999999999822, 0.000000000000000000, 0.000000000000000000 ) ) ;
#837=DIRECTION ( 'NONE',  ( 0.000000000000000000, 1.000000000000000000, 0.000000000000000000 ) ) ;
#958=CIRCLE ( 'NONE', #12845, 0.5249999999999994671 ) ;
#982=FACE_BOUND ( 'NONE', #19326, .T. ) ;
#1014=LINE ( 'NONE', #18140, #17455 ) ;
#1019=CARTESIAN_POINT ( 'NONE',  ( 1.399999999999999911, 13.62500000000000000, 0.000000000000000000 ) ) ;
#1041=CONICAL_SURFACE ( 'NONE', #10948, 18.17500000000000071, 0.7483780475235185525 ) ;
#1061=DIRECTION ( 'NONE',  ( -0.003530072958128175308, -0.9999937692730440641, -1.224639168707530015E-16 ) ) ;
#1074=ORIENTED_EDGE ( 'NONE', *, *, #13658, .F. ) ;
#1111=ORIENTED_EDGE ( 'NONE', *, *, #7761, .F. ) ;
#1130=ORIENTED_EDGE ( 'NONE', *, *, #7791, .F. ) ;
#1156=EDGE_LOOP ( 'NONE', ( #18013, #5005, #16057, #12621 ) ) ;
#1180=EDGE_CURVE ( 'NONE', #4081, #18280, #14650, .T. ) ;
#1184=FACE_OUTER_BOUND ( 'NONE', #17712, .T. ) ;
#1193=CARTESIAN_POINT ( 'NONE',  ( -8.881784197001250351E-16, 0.000000000000000000, 0.000000000000000000 ) ) ;
#1263=CARTESIAN_POINT ( 'NONE',  ( 5.941205806953520074, 0.000000000000000000, 0.000000000000000000 ) ) ;
#1290=AXIS2_PLACEMENT_3D ( 'NONE', #14218, #14029, #13812 ) ;
#1303=AXIS2_PLACEMENT_3D ( 'NONE', #16137, #14674, #546 ) ;
#1305=DIRECTION ( 'NONE',  ( 0.000000000000000000, 1.000000000000000000, 0.000000000000000000 ) ) ;
#1327=ORIENTED_EDGE ( 'NONE', *, *, #2827, .T. ) ;
#1328=FILL_AREA_STYLE_COLOUR ( '', #13365 ) ;
#1357=CYLINDRICAL_SURFACE ( 'NONE', #17501, 15.25000000000000000 ) ;
#1400=CIRCLE ( 'NONE', #15264, 14.76997474683060041 ) ;
#1424=FACE_OUTER_BOUND ( 'NONE', #6660, .T. ) ;
#1453=CONICAL_SURFACE ( 'NONE', #14325, 18.17500000000000071, 0.7483780475235185525 ) ;
#1464=SHAPE_DEFINITION_REPRESENTATION ( #2002, #7605 ) ;
#1546=( NAMED_UNIT ( * ) SI_UNIT ( $, .STERADIAN. ) SOLID_ANGLE_UNIT ( ) );
#1595=CARTESIAN_POINT ( 'NONE',  ( 1.050000000000000044, -15.25000000000000000, -1.867586368699713770E-15 ) ) ;
#1625=AXIS2_PLACEMENT_3D ( 'NONE', #7469, #10642, #16840 ) ;
#1649=CIRCLE ( 'NONE', #7936, 14.76997474683060041 ) ;
#1671=CARTESIAN_POINT ( 'NONE',  ( 7.000000000000000000, 17.68750000000000000, 0.000000000000000000 ) ) ;
#1701=ORIENTED_EDGE ( 'NONE', *, *, #15964, .F. ) ;
#1744=CIRCLE ( 'NONE', #12620, 17.85000000000000142 ) ;
#1745=DIRECTION ( 'NONE',  ( -1.000000000000000000, 0.000000000000000000, 0.000000000000000000 ) ) ;
#1767=ORIENTED_EDGE ( 'NONE', *, *, #8291, .F. ) ;
#1784=DIRECTION ( 'NONE',  ( 0.000000000000000000, 1.000000000000000000, 0.000000000000000000 ) ) ;
#1800=FACE_OUTER_BOUND ( 'NONE', #2407, .T. ) ;
#1811=ORIENTED_EDGE ( 'NONE', *, *, #9123, .T. ) ;
#1845=CARTESIAN_POINT ( 'NONE',  ( 1.050000000000000044, 0.000000000000000000, 0.000000000000000000 ) ) ;
#1873=CONICAL_SURFACE ( 'NONE', #13118, 14.92500000000000071, 1.076854957875310381 ) ;
#1877=ADVANCED_FACE ( 'NONE', ( #6518, #16218 ), #2048, .T. ) ;
#1879=ORIENTED_EDGE ( 'NONE', *, *, #10634, .T. ) ;
#1892=VERTEX_POINT ( 'NONE', #415 ) ;
#1896=CARTESIAN_POINT ( 'NONE',  ( 2.625000000000000000, -14.59999999999999964, -1.787984326755135766E-15 ) ) ;
#1919=EDGE_CURVE ( 'NONE', #18726, #8554, #14848, .T. ) ;
#1929=DIRECTION ( 'NONE',  ( 1.000000000000000000, 0.000000000000000000, 0.000000000000000000 ) ) ;
#1977=CARTESIAN_POINT ( 'NONE',  ( 5.425003271131650706, 0.000000000000000000, 0.000000000000000000 ) ) ;
#2000=CIRCLE ( 'NONE', #6962, 17.52499999999999858 ) ;
#2002=PRODUCT_DEFINITION_SHAPE ( 'NONE', 'NONE',  #2914 ) ;
#2006=EDGE_LOOP ( 'NONE', ( #15847, #2250, #6200, #269 ) ) ;
#2025=ORIENTED_EDGE ( 'NONE', *, *, #6622, .F. ) ;
#2031=LINE ( 'NONE', #19649, #6148 ) ;
#2047=ORIENTED_EDGE ( 'NONE', *, *, #14318, .T. ) ;
#2048=PLANE ( 'NONE',  #18582 ) ;
#2081=EDGE_LOOP ( 'NONE', ( #20014, #11456, #17037, #4517 ) ) ;
#2086=ORIENTED_EDGE ( 'NONE', *, *, #12382, .T. ) ;
#2165=VERTEX_POINT ( 'NONE', #18770 ) ;
#2209=MANIFOLD_SOLID_BREP ( 'Imported1', #8660 ) ;
#2250=ORIENTED_EDGE ( 'NONE', *, *, #7475, .T. ) ;
#2280=EDGE_LOOP ( 'NONE', ( #14129, #18966, #10486, #19919, #6519 ) ) ;
#2390=ORIENTED_EDGE ( 'NONE', *, *, #3879, .F. ) ;
#2407=EDGE_LOOP ( 'NONE', ( #19427, #12874, #9683, #19289 ) ) ;
#2422=ORIENTED_EDGE ( 'NONE', *, *, #7753, .T. ) ;
#2427=EDGE_CURVE ( 'NONE', #8147, #14816, #2799, .T. ) ;
#2446=ADVANCED_FACE ( 'NONE', ( #19669 ), #18620, .T. ) ;
#2452=AXIS2_PLACEMENT_3D ( 'NONE', #18673, #6523, #4562 ) ;
#2474=AXIS2_PLACEMENT_3D ( 'NONE', #16739, #8795, #19589 ) ;
#2515=DIRECTION ( 'NONE',  ( -1.000000000000000000, 0.000000000000000000, 0.000000000000000000 ) ) ;
#2534=ADVANCED_FACE ( 'NONE', ( #12169 ), #9737, .F. ) ;
#2576=ADVANCED_FACE ( 'NONE', ( #11335 ), #12578, .T. ) ;
#2600=ADVANCED_FACE ( 'NONE', ( #11042 ), #12720, .T. ) ;
#2618=VECTOR ( 'NONE', #5705, 1000.000000000000000 ) ;
#2628=CIRCLE ( 'NONE', #13506, 18.50000000000000000 ) ;
#2634=CARTESIAN_POINT ( 'NONE',  ( 1.224999999999999867, 0.000000000000000000, 0.000000000000000000 ) ) ;
#2656=DIRECTION ( 'NONE',  ( 1.000000000000000000, 0.000000000000000000, 0.000000000000000000 ) ) ;
#2663=LINE ( 'NONE', #7428, #3839 ) ;
#2694=EDGE_CURVE ( 'NONE', #6321, #14904, #15352, .T. ) ;
#2703=ORIENTED_EDGE ( 'NONE', *, *, #7218, .F. ) ;
#2735=CARTESIAN_POINT ( 'NONE',  ( 5.945602903476760126, -13.89560290347679938, -1.701720561796553076E-15 ) ) ;
#2741=AXIS2_PLACEMENT_3D ( 'NONE', #5042, #3500, #8234 ) ;
#2771=CIRCLE ( 'NONE', #2452, 15.14120580695350071 ) ;
#2774=VERTEX_POINT ( 'NONE', #17817 ) ;
#2791=ADVANCED_FACE ( 'NONE', ( #13115 ), #8117, .T. ) ;
#2799=CIRCLE ( 'NONE', #20262, 13.95000000000000107 ) ;
#2801=EDGE_CURVE ( 'NONE', #5440, #6498, #2031, .T. ) ;
#2827=EDGE_CURVE ( 'NONE', #9164, #2774, #9756, .T. ) ;
#2829=CARTESIAN_POINT ( 'NONE',  ( 5.687501635565830327, 0.000000000000000000, 0.000000000000000000 ) ) ;
#2879=CARTESIAN_POINT ( 'NONE',  ( -8.881784197001250351E-16, 17.85000000000000142, 0.000000000000000000 ) ) ;
#2914=PRODUCT_DEFINITION ( 'UNKNOWN', '', #13905, #18103 ) ;
#2956=DIRECTION ( 'NONE',  ( 0.000000000000000000, 0.000000000000000000, -1.000000000000000000 ) ) ;
#3017=PRODUCT_CONTEXT ( 'NONE', #15534, 'mechanical' ) ;
#3051=ORIENTED_EDGE ( 'NONE', *, *, #16596, .F. ) ;
#3069=AXIS2_PLACEMENT_3D ( 'NONE', #8875, #13618, #18346 ) ;
#3118=DIRECTION ( 'NONE',  ( 0.000000000000000000, 1.000000000000000000, 0.000000000000000000 ) ) ;
#3164=DIRECTION ( 'NONE',  ( 0.000000000000000000, 1.000000000000000000, 0.000000000000000000 ) ) ;
#3166=DIRECTION ( 'NONE',  ( 0.000000000000000000, 1.000000000000000000, 0.000000000000000000 ) ) ;
#3185=CARTESIAN_POINT ( 'NONE',  ( 3.500000000000000000, 0.000000000000000000, 0.000000000000000000 ) ) ;
#3247=ADVANCED_FACE ( 'NONE', ( #20026 ), #1357, .T. ) ;
#3270=CIRCLE ( 'NONE', #16498, 15.25000000000000000 ) ;
#3303=DIRECTION ( 'NONE',  ( -1.000000000000000000, 0.000000000000000000, 0.000000000000000000 ) ) ;
#3362=CIRCLE ( 'NONE', #8313, 0.6999999999999992895 ) ;
#3370=ORIENTED_EDGE ( 'NONE', *, *, #6922, .F. ) ;
#3379=ADVANCED_FACE ( 'NONE', ( #7886 ), #6016, .T. ) ;
#3409=DIRECTION ( 'NONE',  ( 1.000000000000000000, 0.000000000000000000, 0.000000000000000000 ) ) ;
#3448=FACE_OUTER_BOUND ( 'NONE', #14593, .T. ) ;
#3500=DIRECTION ( 'NONE',  ( 0.000000000000000000, 0.000000000000000000, 1.000000000000000000 ) ) ;
#3616=DIRECTION ( 'NONE',  ( 1.000000000000000000, 0.000000000000000000, 0.000000000000000000 ) ) ;
#3618=LINE ( 'NONE', #19280, #7825 ) ;
#3624=CARTESIAN_POINT ( 'NONE',  ( 5.162501635565829972, 0.000000000000000000, 0.000000000000000000 ) ) ;
#3649=AXIS2_PLACEMENT_3D ( 'NONE', #7984, #2656, #12744 ) ;
#3657=LINE ( 'NONE', #12079, #16330 ) ;
#3699=ADVANCED_FACE ( 'NONE', ( #19361 ), #1873, .T. ) ;
#3703=ORIENTED_EDGE ( 'NONE', *, *, #7005, .T. ) ;
#3773=EDGE_LOOP ( 'NONE', ( #12751, #2703, #7272, #19122, #17170 ) ) ;
#3779=AXIS2_PLACEMENT_3D ( 'NONE', #17330, #17223, #9490 ) ;
#3809=ORIENTED_EDGE ( 'NONE', *, *, #5580, .F. ) ;
#3810=ORIENTED_EDGE ( 'NONE', *, *, #14053, .T. ) ;
#3811=EDGE_CURVE ( 'NONE', #14904, #15622, #3618, .T. ) ;
#3839=VECTOR ( 'NONE', #13791, 1000.000000000000227 ) ;
#3879=EDGE_CURVE ( 'NONE', #4081, #10815, #11856, .T. ) ;
#3898=FACE_OUTER_BOUND ( 'NONE', #4437, .T. ) ;
#3921=EDGE_LOOP ( 'NONE', ( #7354, #4003, #11072, #8822 ) ) ;
#4003=ORIENTED_EDGE ( 'NONE', *, *, #12093, .T. ) ;
#4023=ORIENTED_EDGE ( 'NONE', *, *, #17792, .T. ) ;
#4036=DIRECTION ( 'NONE',  ( 0.000000000000000000, 1.000000000000000000, 0.000000000000000000 ) ) ;
#4043=CARTESIAN_POINT ( 'NONE',  ( 1.574999999999999956, 0.000000000000000000, 0.000000000000000000 ) ) ;
#4045=FACE_OUTER_BOUND ( 'NONE', #2081, .T. ) ;
#4047=ORIENTED_EDGE ( 'NONE', *, *, #20246, .T. ) ;
#4061=CARTESIAN_POINT ( 'NONE',  ( 1.224999999999999867, 15.25000000000000000, 0.000000000000000000 ) ) ;
#4081=VERTEX_POINT ( 'NONE', #282 ) ;
#4118=ORIENTED_EDGE ( 'NONE', *, *, #7761, .T. ) ;
#4127=AXIS2_PLACEMENT_3D ( 'NONE', #702, #5937, #9028 ) ;
#4134=AXIS2_PLACEMENT_3D ( 'NONE', #650, #9841, #8411 ) ;
#4158=DIRECTION ( 'NONE',  ( 1.000000000000000000, 0.000000000000000000, 0.000000000000000000 ) ) ;
#4190=VERTEX_POINT ( 'NONE', #12878 ) ;
#4202=VECTOR ( 'NONE', #10410, 1000.000000000000000 ) ;
#4234=DIRECTION ( 'NONE',  ( 0.000000000000000000, 1.000000000000000000, 0.000000000000000000 ) ) ;
#4287=AXIS2_PLACEMENT_3D ( 'NONE', #13654, #9004, #10152 ) ;
#4288=VECTOR ( 'NONE', #10981, 1000.000000000000000 ) ;
#4295=DIRECTION ( 'NONE',  ( 1.000000000000000000, 0.000000000000000000, 0.000000000000000000 ) ) ;
#4320=DIRECTION ( 'NONE',  ( 0.000000000000000000, 1.000000000000000000, 0.000000000000000000 ) ) ;
#4335=EDGE_CURVE ( 'NONE', #11484, #19448, #16409, .T. ) ;
#4351=CARTESIAN_POINT ( 'NONE',  ( 5.941205806953520074, 15.14120580695428764, 0.000000000000000000 ) ) ;
#4365=EDGE_LOOP ( 'NONE', ( #8882, #117, #14257, #11121 ) ) ;
#4401=VECTOR ( 'NONE', #14700, 1000.000000000000000 ) ;
#4418=DIRECTION ( 'NONE',  ( 0.000000000000000000, 1.000000000000000000, 0.000000000000000000 ) ) ;
#4425=AXIS2_PLACEMENT_3D ( 'NONE', #10801, #17082, #2956 ) ;
#4437=EDGE_LOOP ( 'NONE', ( #15197, #4867, #11819, #2390 ) ) ;
#4473=AXIS2_PLACEMENT_3D ( 'NONE', #5260, #1929, #11125 ) ;
#4489=AXIS2_PLACEMENT_3D ( 'NONE', #14738, #10103, #11854 ) ;
#4517=ORIENTED_EDGE ( 'NONE', *, *, #19290, .F. ) ;
#4562=DIRECTION ( 'NONE',  ( 0.000000000000000000, 1.000000000000000000, 0.000000000000000000 ) ) ;
#4592=ADVANCED_FACE ( 'NONE', ( #1800 ), #20347, .F. ) ;
#4614=CARTESIAN_POINT ( 'NONE',  ( 3.500000000000000000, -14.59999999999999964, -1.787984326755135766E-15 ) ) ;
#4637=ORIENTED_EDGE ( 'NONE', *, *, #5992, .F. ) ;
#4641=EDGE_LOOP ( 'NONE', ( #9935, #1111, #1811, #19493 ) ) ;
#4655=CARTESIAN_POINT ( 'NONE',  ( 3.850000000000000089, 1.778491767751089605E-15, 14.27500000000000036 ) ) ;
#4663=SURFACE_STYLE_FILL_AREA ( #7657 ) ;
#4683=( GEOMETRIC_REPRESENTATION_CONTEXT ( 3 ) GLOBAL_UNCERTAINTY_ASSIGNED_CONTEXT ( ( #19743 ) ) GLOBAL_UNIT_ASSIGNED_CONTEXT ( ( #11620, #9875, #11736 ) ) REPRESENTATION_CONTEXT ( 'NONE', 'WORKASPACE' ) );
#4720=AXIS2_PLACEMENT_3D ( 'NONE', #19136, #11018, #12561 ) ;
#4790=DIRECTION ( 'NONE',  ( 0.000000000000000000, 1.000000000000000000, 0.000000000000000000 ) ) ;
#4802=FACE_OUTER_BOUND ( 'NONE', #3921, .T. ) ;
#4805=PLANE ( 'NONE',  #16174 ) ;
#4806=CONICAL_SURFACE ( 'NONE', #17300, 12.64907335584850046, 0.003530080289784348537 ) ;
#4809=DIRECTION ( 'NONE',  ( 0.000000000000000000, 0.000000000000000000, -1.000000000000000000 ) ) ;
#4810=DIRECTION ( 'NONE',  ( 1.000000000000000000, 0.000000000000000000, 0.000000000000000000 ) ) ;
#4827=CARTESIAN_POINT ( 'NONE',  ( 1.399999999999999911, -15.25000000000000000, -1.867586368699713770E-15 ) ) ;
#4846=ORIENTED_EDGE ( 'NONE', *, *, #16216, .F. ) ;
#4852=DIRECTION ( 'NONE',  ( 1.000000000000000000, 0.000000000000000000, 0.000000000000000000 ) ) ;
#4867=ORIENTED_EDGE ( 'NONE', *, *, #14743, .T. ) ;
#4889=ORIENTED_EDGE ( 'NONE', *, *, #1180, .F. ) ;
#4942=ADVANCED_FACE ( 'NONE', ( #14059 ), #10157, .F. ) ;
#5005=ORIENTED_EDGE ( 'NONE', *, *, #13421, .T. ) ;
#5008=DIRECTION ( 'NONE',  ( 0.000000000000000000, 0.000000000000000000, -1.000000000000000000 ) ) ;
#5042=CARTESIAN_POINT ( 'NONE',  ( 0.000000000000000000, 0.000000000000000000, 0.000000000000000000 ) ) ;
#5044=CARTESIAN_POINT ( 'NONE',  ( 6.649999999999999467, 0.000000000000000000, 0.000000000000000000 ) ) ;
#5047=CONICAL_SURFACE ( 'NONE', #14235, 14.43750000000000000, 0.7483780475235185525 ) ;
#5064=CARTESIAN_POINT ( 'NONE',  ( 3.500000000000000000, 0.000000000000000000, 0.000000000000000000 ) ) ;
#5080=CARTESIAN_POINT ( 'NONE',  ( 2.625000000000000000, 0.000000000000000000, 0.000000000000000000 ) ) ;
#5151=AXIS2_PLACEMENT_3D ( 'NONE', #11565, #4158, #17948 ) ;
#5156=AXIS2_PLACEMENT_3D ( 'NONE', #1977, #12948, #5793 ) ;
#5173=CARTESIAN_POINT ( 'NONE',  ( 1.750000000000000000, 0.000000000000000000, 0.000000000000000000 ) ) ;
#5220=VERTEX_POINT ( 'NONE', #11212 ) ;
#5245=CARTESIAN_POINT ( 'NONE',  ( 0.6999999999999999556, 0.000000000000000000, 0.000000000000000000 ) ) ;
#5260=CARTESIAN_POINT ( 'NONE',  ( 7.000000000000000000, 0.000000000000000000, 0.000000000000000000 ) ) ;
#5268=APPLICATION_CONTEXT ( 'automotive_design' ) ;
#5379=DIRECTION ( 'NONE',  ( 0.000000000000000000, 1.000000000000000000, 0.000000000000000000 ) ) ;
#5422=ORIENTED_EDGE ( 'NONE', *, *, #19187, .T. ) ;
#5440=VERTEX_POINT ( 'NONE', #18002 ) ;
#5443=VECTOR ( 'NONE', #11902, 1000.000000000000227 ) ;
#5446=CARTESIAN_POINT ( 'NONE',  ( 3.850000000000000089, 0.000000000000000000, 0.000000000000000000 ) ) ;
#5457=CIRCLE ( 'NONE', #12054, 14.59999999999999964 ) ;
#5494=CARTESIAN_POINT ( 'NONE',  ( -1.776356839400249676E-15, -13.94999999999999929, -1.708382284810557762E-15 ) ) ;
#5496=DIRECTION ( 'NONE',  ( 0.7327934916262990317, -0.6804510993672779895, 8.333122608164345406E-17 ) ) ;
#5515=DIRECTION ( 'NONE',  ( -1.000000000000000000, 0.000000000000000000, 0.000000000000000000 ) ) ;
#5526=ORIENTED_EDGE ( 'NONE', *, *, #7218, .T. ) ;
#5527=AXIS2_PLACEMENT_3D ( 'NONE', #5245, #13187, #682 ) ;
#5557=DIRECTION ( 'NONE',  ( 0.000000000000000000, 0.000000000000000000, -1.000000000000000000 ) ) ;
#5580=EDGE_CURVE ( 'NONE', #18077, #1892, #18272, .T. ) ;
#5605=LINE ( 'NONE', #15398, #5443 ) ;
#5627=AXIS2_PLACEMENT_3D ( 'NONE', #529, #16421, #718 ) ;
#5629=VERTEX_POINT ( 'NONE', #7068 ) ;
#5673=ORIENTED_EDGE ( 'NONE', *, *, #1180, .T. ) ;
#5705=DIRECTION ( 'NONE',  ( -1.000000000000000000, 0.000000000000000000, 0.000000000000000000 ) ) ;
#5721=AXIS2_PLACEMENT_3D ( 'NONE', #19096, #247, #6549 ) ;
#5731=ADVANCED_FACE ( 'NONE', ( #19601 ), #14574, .T. ) ;
#5740=VECTOR ( 'NONE', #18633, 1000.000000000000227 ) ;
#5793=DIRECTION ( 'NONE',  ( 0.000000000000000000, 1.000000000000000000, 0.000000000000000000 ) ) ;
#5847=DIRECTION ( 'NONE',  ( -0.003530072958128175308, 0.9999937692730440641, 0.000000000000000000 ) ) ;
#5924=ORIENTED_EDGE ( 'NONE', *, *, #16719, .T. ) ;
#5937=DIRECTION ( 'NONE',  ( 1.000000000000000000, 0.000000000000000000, 0.000000000000000000 ) ) ;
#5941=CARTESIAN_POINT ( 'NONE',  ( 1.399999999999999911, 15.25000000000000000, 0.000000000000000000 ) ) ;
#5960=EDGE_CURVE ( 'NONE', #18280, #4081, #16804, .T. ) ;
#5965=AXIS2_PLACEMENT_3D ( 'NONE', #8966, #15266, #1305 ) ;
#5992=EDGE_CURVE ( 'NONE', #15525, #5440, #11531, .T. ) ;
#6010=EDGE_LOOP ( 'NONE', ( #13835, #14000, #18533, #19877 ) ) ;
#6016=TOROIDAL_SURFACE ( 'NONE', #8003, 14.76997474683060041, 0.5250000000000000222 ) ;
#6075=AXIS2_PLACEMENT_3D ( 'NONE', #11575, #16138, #16434 ) ;
#6127=SURFACE_SIDE_STYLE ('',( #4663 ) ) ;
#6129=AXIS2_PLACEMENT_3D ( 'NONE', #5064, #18955, #6611 ) ;
#6148=VECTOR ( 'NONE', #11755, 1000.000000000000000 ) ;
#6151=CARTESIAN_POINT ( 'NONE',  ( 1.750000000000000000, 0.000000000000000000, 0.000000000000000000 ) ) ;
#6167=CARTESIAN_POINT ( 'NONE',  ( 3.674999999999999822, 0.000000000000000000, 0.000000000000000000 ) ) ;
#6200=ORIENTED_EDGE ( 'NONE', *, *, #6622, .T. ) ;
#6212=DIRECTION ( 'NONE',  ( 0.7327934916262990317, 0.6804510993672779895, 0.000000000000000000 ) ) ;
#6258=EDGE_CURVE ( 'NONE', #15622, #13610, #17746, .T. ) ;
#6285=FACE_OUTER_BOUND ( 'NONE', #3773, .T. ) ;
#6301=CARTESIAN_POINT ( 'NONE',  ( 5.044974746830580337, 0.000000000000000000, 0.000000000000000000 ) ) ;
#6321=VERTEX_POINT ( 'NONE', #17502 ) ;
#6354=CARTESIAN_POINT ( 'NONE',  ( 5.569974746830579804, 0.000000000000000000, 0.000000000000000000 ) ) ;
#6422=CARTESIAN_POINT ( 'NONE',  ( 4.025000000000000355, -17.52499999999999858, -2.146193515505736390E-15 ) ) ;
#6447=VECTOR ( 'NONE', #7266, 1000.000000000000000 ) ;
#6453=DIRECTION ( 'NONE',  ( -6.123031769111888756E-17, -1.000000000000000000, 0.000000000000000000 ) ) ;
#6466=DIRECTION ( 'NONE',  ( 0.000000000000000000, 1.000000000000000000, 0.000000000000000000 ) ) ;
#6498=VERTEX_POINT ( 'NONE', #11954 ) ;
#6499=DIRECTION ( 'NONE',  ( 0.000000000000000000, 1.000000000000000000, 0.000000000000000000 ) ) ;
#6508=DIRECTION ( 'NONE',  ( 0.000000000000000000, 1.000000000000000000, 0.000000000000000000 ) ) ;
#6518=FACE_BOUND ( 'NONE', #12788, .T. ) ;
#6519=ORIENTED_EDGE ( 'NONE', *, *, #7005, .F. ) ;
#6523=DIRECTION ( 'NONE',  ( 1.000000000000000000, 0.000000000000000000, 0.000000000000000000 ) ) ;
#6536=AXIS2_PLACEMENT_3D ( 'NONE', #17572, #9532, #7996 ) ;
#6549=DIRECTION ( 'NONE',  ( 0.000000000000000000, 1.000000000000000000, 0.000000000000000000 ) ) ;
#6597=AXIS2_PLACEMENT_3D ( 'NONE', #9192, #20109, #17338 ) ;
#6611=DIRECTION ( 'NONE',  ( 0.000000000000000000, 1.000000000000000000, 0.000000000000000000 ) ) ;
#6622=EDGE_CURVE ( 'NONE', #19448, #11484, #2628, .T. ) ;
#6638=CIRCLE ( 'NONE', #13540, 12.00000000000000000 ) ;
#6660=EDGE_LOOP ( 'NONE', ( #18371, #14421, #12114, #13758 ) ) ;
#6663=CARTESIAN_POINT ( 'NONE',  ( 1.224999999999999867, 0.000000000000000000, 0.000000000000000000 ) ) ;
#6667=FACE_OUTER_BOUND ( 'NONE', #9431, .T. ) ;
#6706=CIRCLE ( 'NONE', #16907, 14.59999999999999964 ) ;
#6779=CARTESIAN_POINT ( 'NONE',  ( 6.649999999999999467, 0.000000000000000000, 0.000000000000000000 ) ) ;
#6851=CARTESIAN_POINT ( 'NONE',  ( 3.324999999999999734, 12.97499999999999964, 0.000000000000000000 ) ) ;
#6881=EDGE_CURVE ( 'NONE', #2165, #15076, #18609, .T. ) ;
#6922=EDGE_CURVE ( 'NONE', #6498, #13953, #12434, .T. ) ;
#6930=DIRECTION ( 'NONE',  ( 0.000000000000000000, 1.000000000000000000, 0.000000000000000000 ) ) ;
#6936=CIRCLE ( 'NONE', #19407, 0.5249999999999994671 ) ;
#6939=LINE ( 'NONE', #16631, #9558 ) ;
#6962=AXIS2_PLACEMENT_3D ( 'NONE', #1845, #205, #8156 ) ;
#7003=DIRECTION ( 'NONE',  ( 1.000000000000000000, 0.000000000000000000, 0.000000000000000000 ) ) ;
#7005=EDGE_CURVE ( 'NONE', #19679, #19612, #6936, .T. ) ;
#7068=CARTESIAN_POINT ( 'NONE',  ( 5.425003271131650706, -12.64814671169700055, 1.549064719741994274E-15 ) ) ;
#7087=VECTOR ( 'NONE', #15057, 1000.000000000000000 ) ;
#7122=CIRCLE ( 'NONE', #5156, 12.64814671169700055 ) ;
#7151=CARTESIAN_POINT ( 'NONE',  ( 1.750000000000000000, 14.59999999999999964, 0.000000000000000000 ) ) ;
#7169=ORIENTED_EDGE ( 'NONE', *, *, #2694, .F. ) ;
#7191=ADVANCED_FACE ( 'NONE', ( #982, #15354 ), #4805, .T. ) ;
#7218=EDGE_CURVE ( 'NONE', #19306, #18726, #9895, .T. ) ;
#7219=CARTESIAN_POINT ( 'NONE',  ( 6.649999999999999467, 18.17500000000000071, 0.000000000000000000 ) ) ;
#7266=DIRECTION ( 'NONE',  ( -0.7327934916262990317, -0.6804510993672779895, -8.333122608164345406E-17 ) ) ;
#7269=CONICAL_SURFACE ( 'NONE', #20066, 12.97499999999999964, 0.5543074962015517304 ) ;
#7272=ORIENTED_EDGE ( 'NONE', *, *, #10634, .F. ) ;
#7283=EDGE_CURVE ( 'NONE', #19679, #4190, #1649, .T. ) ;
#7327=ORIENTED_EDGE ( 'NONE', *, *, #17792, .F. ) ;
#7334=ADVANCED_FACE ( 'NONE', ( #9708 ), #19178, .T. ) ;
#7337=VECTOR ( 'NONE', #15842, 1000.000000000000114 ) ;
#7354=ORIENTED_EDGE ( 'NONE', *, *, #9483, .F. ) ;
#7392=EDGE_CURVE ( 'NONE', #19303, #15899, #11889, .T. ) ;
#7418=ORIENTED_EDGE ( 'NONE', *, *, #15149, .F. ) ;
#7428=CARTESIAN_POINT ( 'NONE',  ( 5.687501635565830327, -12.64907335584850046, 1.549064719741993485E-15 ) ) ;
#7469=CARTESIAN_POINT ( 'NONE',  ( 7.000000000000000000, 0.000000000000000000, 0.000000000000000000 ) ) ;
#7475=EDGE_CURVE ( 'NONE', #17493, #19448, #6939, .T. ) ;
#7494=DIRECTION ( 'NONE',  ( -1.000000000000000000, 0.000000000000000000, 0.000000000000000000 ) ) ;
#7521=DIRECTION ( 'NONE',  ( 1.000000000000000000, 0.000000000000000000, 0.000000000000000000 ) ) ;
#7531=ADVANCED_FACE ( 'NONE', ( #12167 ), #10824, .T. ) ;
#7580=CONICAL_SURFACE ( 'NONE', #9560, 14.92500000000000071, 1.076854957875310381 ) ;
#7584=DIRECTION ( 'NONE',  ( 0.000000000000000000, 1.000000000000000000, 0.000000000000000000 ) ) ;
#7605=SHAPE_REPRESENTATION ( '722909', ( #2741 ), #4683 ) ;
#7635=DIRECTION ( 'NONE',  ( 1.000000000000000000, 0.000000000000000000, 0.000000000000000000 ) ) ;
#7657=FILL_AREA_STYLE ('',( #1328 ) ) ;
#7698=CARTESIAN_POINT ( 'NONE',  ( 1.399999999999999911, 0.000000000000000000, 0.000000000000000000 ) ) ;
#7753=EDGE_CURVE ( 'NONE', #13610, #15622, #2000, .T. ) ;
#7761=EDGE_CURVE ( 'NONE', #13085, #15933, #6638, .T. ) ;
#7791=EDGE_CURVE ( 'NONE', #4190, #19679, #1400, .T. ) ;
#7825=VECTOR ( 'NONE', #8254, 1000.000000000000000 ) ;
#7852=DIRECTION ( 'NONE',  ( 0.000000000000000000, 1.000000000000000000, 0.000000000000000000 ) ) ;
#7886=FACE_OUTER_BOUND ( 'NONE', #2280, .T. ) ;
#7921=DIRECTION ( 'NONE',  ( 1.000000000000000000, 0.000000000000000000, 0.000000000000000000 ) ) ;
#7936=AXIS2_PLACEMENT_3D ( 'NONE', #14349, #17230, #3118 ) ;
#7948=CARTESIAN_POINT ( 'NONE',  ( 0.3499999999999999778, 18.17500000000000071, 0.000000000000000000 ) ) ;
#7984=CARTESIAN_POINT ( 'NONE',  ( 3.850000000000000089, 0.000000000000000000, 0.000000000000000000 ) ) ;
#7996=DIRECTION ( 'NONE',  ( 0.000000000000000000, 1.000000000000000000, 0.000000000000000000 ) ) ;
#8003=AXIS2_PLACEMENT_3D ( 'NONE', #6354, #18906, #4809 ) ;
#8013=DIRECTION ( 'NONE',  ( 0.000000000000000000, 1.000000000000000000, 0.000000000000000000 ) ) ;
#8039=ORIENTED_EDGE ( 'NONE', *, *, #14743, .F. ) ;
#8050=TOROIDAL_SURFACE ( 'NONE', #4425, 14.76997474683060041, 0.5250000000000000222 ) ;
#8064=DIRECTION ( 'NONE',  ( 1.000000000000000000, 0.000000000000000000, 0.000000000000000000 ) ) ;
#8074=AXIS2_PLACEMENT_3D ( 'NONE', #6779, #19406, #8417 ) ;
#8093=VERTEX_POINT ( 'NONE', #1595 ) ;
#8117=TOROIDAL_SURFACE ( 'NONE', #18632, 14.27500000000000036, 0.6999999999999999556 ) ;
#8147=VERTEX_POINT ( 'NONE', #14804 ) ;
#8156=DIRECTION ( 'NONE',  ( 0.000000000000000000, 1.000000000000000000, 0.000000000000000000 ) ) ;
#8158=CARTESIAN_POINT ( 'NONE',  ( 4.549999999999999822, 0.000000000000000000, 0.000000000000000000 ) ) ;
#8202=DIRECTION ( 'NONE',  ( -1.000000000000000000, 0.000000000000000000, 0.000000000000000000 ) ) ;
#8206=CARTESIAN_POINT ( 'NONE',  ( 1.750000000000000000, -14.59999999999999964, -1.827785347727424768E-15 ) ) ;
#8234=DIRECTION ( 'NONE',  ( 1.000000000000000000, 0.000000000000000000, 0.000000000000000000 ) ) ;
#8254=DIRECTION ( 'NONE',  ( -1.000000000000000000, 0.000000000000000000, 0.000000000000000000 ) ) ;
#8289=DIRECTION ( 'NONE',  ( 0.000000000000000000, 0.000000000000000000, 1.000000000000000000 ) ) ;
#8291=EDGE_CURVE ( 'NONE', #19306, #4190, #14896, .T. ) ;
#8313=AXIS2_PLACEMENT_3D ( 'NONE', #15199, #10658, #12202 ) ;
#8321=ORIENTED_EDGE ( 'NONE', *, *, #8328, .F. ) ;
#8328=EDGE_CURVE ( 'NONE', #15933, #9164, #10877, .T. ) ;
#8354=AXIS2_PLACEMENT_3D ( 'NONE', #101, #3303, #10732 ) ;
#8389=AXIS2_PLACEMENT_3D ( 'NONE', #3624, #13017, #6930 ) ;
#8411=DIRECTION ( 'NONE',  ( 0.000000000000000000, 1.000000000000000000, 0.000000000000000000 ) ) ;
#8417=DIRECTION ( 'NONE',  ( 0.000000000000000000, 1.000000000000000000, 0.000000000000000000 ) ) ;
#8418=CARTESIAN_POINT ( 'NONE',  ( 5.945602903476760126, 0.000000000000000000, 0.000000000000000000 ) ) ;
#8446=LINE ( 'NONE', #9781, #719 ) ;
#8498=FACE_OUTER_BOUND ( 'NONE', #18838, .T. ) ;
#8554=VERTEX_POINT ( 'NONE', #4614 ) ;
#8577=VERTEX_POINT ( 'NONE', #4827 ) ;
#8660=CLOSED_SHELL ( 'NONE', ( #3379, #2791, #14429, #13055, #4942, #15934, #9121, #58, #13668, #7531, #3699, #5731, #14038, #13406, #13947, #18026, #1877, #7191, #2576, #14544, #4592, #3247, #19920, #7334, #20311, #11046, #8985, #2534, #19996, #19327, #2446, #2600, #705 ) ) ;
#8703=ORIENTED_EDGE ( 'NONE', *, *, #187, .F. ) ;
#8722=VECTOR ( 'NONE', #15798, 1000.000000000000000 ) ;
#8792=CARTESIAN_POINT ( 'NONE',  ( 7.000000000000000000, 17.52499999999999858, 0.000000000000000000 ) ) ;
#8795=DIRECTION ( 'NONE',  ( -1.000000000000000000, 0.000000000000000000, 0.000000000000000000 ) ) ;
#8822=ORIENTED_EDGE ( 'NONE', *, *, #14053, .F. ) ;
#8875=CARTESIAN_POINT ( 'NONE',  ( 5.950000000000000178, 0.000000000000000000, 0.000000000000000000 ) ) ;
#8882=ORIENTED_EDGE ( 'NONE', *, *, #9011, .F. ) ;
#8915=AXIS2_PLACEMENT_3D ( 'NONE', #5080, #15803, #7852 ) ;
#8966=CARTESIAN_POINT ( 'NONE',  ( 2.625000000000000000, 0.000000000000000000, 0.000000000000000000 ) ) ;
#8985=ADVANCED_FACE ( 'NONE', ( #16971 ), #4806, .F. ) ;
#8990=AXIS2_PLACEMENT_3D ( 'NONE', #11646, #17819, #14526 ) ;
#9004=DIRECTION ( 'NONE',  ( 1.000000000000000000, 0.000000000000000000, 0.000000000000000000 ) ) ;
#9011=EDGE_CURVE ( 'NONE', #12573, #13953, #5457, .T. ) ;
#9028=DIRECTION ( 'NONE',  ( 0.000000000000000000, 1.000000000000000000, 0.000000000000000000 ) ) ;
#9088=DIRECTION ( 'NONE',  ( 0.000000000000000000, 1.000000000000000000, 0.000000000000000000 ) ) ;
#9094=AXIS2_PLACEMENT_3D ( 'NONE', #9481, #3616, #17722 ) ;
#9121=ADVANCED_FACE ( 'NONE', ( #4802 ), #10083, .F. ) ;
#9123=EDGE_CURVE ( 'NONE', #13085, #5220, #3657, .T. ) ;
#9139=EDGE_CURVE ( 'NONE', #5220, #5629, #7122, .T. ) ;
#9164=VERTEX_POINT ( 'NONE', #14683 ) ;
#9192=CARTESIAN_POINT ( 'NONE',  ( 3.850000000000000089, 0.000000000000000000, 0.000000000000000000 ) ) ;
#9208=ORIENTED_EDGE ( 'NONE', *, *, #20246, .F. ) ;
#9359=ADVANCED_BREP_SHAPE_REPRESENTATION ( '', ( #2209, #2741 ), #4683 ) ;
#9392=LINE ( 'NONE', #12580, #14929 ) ;
#9408=AXIS2_PLACEMENT_3D ( 'NONE', #8158, #3409, #17629 ) ;
#9427=EDGE_CURVE ( 'NONE', #14904, #6321, #13381, .T. ) ;
#9431=EDGE_LOOP ( 'NONE', ( #4047, #14372, #15414, #11748 ) ) ;
#9470=EDGE_CURVE ( 'NONE', #9164, #14816, #17315, .T. ) ;
#9481=CARTESIAN_POINT ( 'NONE',  ( 7.000000000000000000, 0.000000000000000000, 0.000000000000000000 ) ) ;
#9483=EDGE_CURVE ( 'NONE', #5629, #5220, #18637, .T. ) ;
#9490=DIRECTION ( 'NONE',  ( 0.000000000000000000, 1.000000000000000000, 0.000000000000000000 ) ) ;
#9532=DIRECTION ( 'NONE',  ( -1.000000000000000000, 0.000000000000000000, 0.000000000000000000 ) ) ;
#9558=VECTOR ( 'NONE', #15064, 1000.000000000000000 ) ;
#9560=AXIS2_PLACEMENT_3D ( 'NONE', #4043, #18043, #16643 ) ;
#9572=DIRECTION ( 'NONE',  ( 1.000000000000000000, 0.000000000000000000, 0.000000000000000000 ) ) ;
#9606=EDGE_LOOP ( 'NONE', ( #1879, #13427, #18175, #7327, #13152 ) ) ;
#9663=CIRCLE ( 'NONE', #17557, 14.27500000000000036 ) ;
#9683=ORIENTED_EDGE ( 'NONE', *, *, #3811, .T. ) ;
#9704=ORIENTED_EDGE ( 'NONE', *, *, #12398, .T. ) ;
#9708=FACE_OUTER_BOUND ( 'NONE', #6010, .T. ) ;
#9718=EDGE_CURVE ( 'NONE', #2774, #9164, #13086, .T. ) ;
#9737=CONICAL_SURFACE ( 'NONE', #19924, 12.32407335584850117, 0.8899833664651138898 ) ;
#9755=LINE ( 'NONE', #1896, #4401 ) ;
#9756=CIRCLE ( 'NONE', #4489, 13.29999999999999893 ) ;
#9781=CARTESIAN_POINT ( 'NONE',  ( 5.162501635565829972, -12.32407335584850117, 1.509263698769704680E-15 ) ) ;
#9810=EDGE_LOOP ( 'NONE', ( #16076, #16849, #16419, #14681 ) ) ;
#9841=DIRECTION ( 'NONE',  ( 1.000000000000000000, 0.000000000000000000, 0.000000000000000000 ) ) ;
#9861=CARTESIAN_POINT ( 'NONE',  ( 2.799999999999999822, 0.000000000000000000, 0.000000000000000000 ) ) ;
#9875=( NAMED_UNIT ( * ) PLANE_ANGLE_UNIT ( ) SI_UNIT ( $, .RADIAN. ) );
#9892=AXIS2_PLACEMENT_3D ( 'NONE', #3185, #7921, #10918 ) ;
#9895=CIRCLE ( 'NONE', #3649, 14.27500000000000036 ) ;
#9935=ORIENTED_EDGE ( 'NONE', *, *, #13421, .F. ) ;
#10068=AXIS2_PLACEMENT_3D ( 'NONE', #11078, #15937, #1784 ) ;
#10083=CONICAL_SURFACE ( 'NONE', #10068, 12.64907335584850046, 0.003530080289784348537 ) ;
#10103=DIRECTION ( 'NONE',  ( 1.000000000000000000, 0.000000000000000000, 0.000000000000000000 ) ) ;
#10152=DIRECTION ( 'NONE',  ( 0.000000000000000000, 1.000000000000000000, 0.000000000000000000 ) ) ;
#10157=CONICAL_SURFACE ( 'NONE', #603, 12.97499999999999964, 0.5543074962015517304 ) ;
#10173=DIRECTION ( 'NONE',  ( -1.000000000000000000, 0.000000000000000000, 0.000000000000000000 ) ) ;
#10216=CYLINDRICAL_SURFACE ( 'NONE', #17544, 18.50000000000000000 ) ;
#10282=EDGE_LOOP ( 'NONE', ( #5673, #321 ) ) ;
#10309=ORIENTED_EDGE ( 'NONE', *, *, #5580, .T. ) ;
#10325=CARTESIAN_POINT ( 'NONE',  ( 0.6999999999999999556, 18.50000000000000000, 0.000000000000000000 ) ) ;
#10331=CIRCLE ( 'NONE', #13637, 12.65000000000000036 ) ;
#10350=LINE ( 'NONE', #16662, #488 ) ;
#10373=ORIENTED_EDGE ( 'NONE', *, *, #11411, .F. ) ;
#10392=CARTESIAN_POINT ( 'NONE',  ( 6.299999999999999822, -18.50000000000000000, -2.265596578422603396E-15 ) ) ;
#10410=DIRECTION ( 'NONE',  ( -0.7327934916262990317, 0.6804510993672779895, 0.000000000000000000 ) ) ;
#10440=EDGE_CURVE ( 'NONE', #19612, #19303, #2771, .T. ) ;
#10486=ORIENTED_EDGE ( 'NONE', *, *, #7392, .F. ) ;
#10576=LINE ( 'NONE', #19832, #19213 ) ;
#10580=SHAPE_REPRESENTATION_RELATIONSHIP ( 'NONE' , 'NONE' ,  #7605, #9359 ) ;
#10603=DIRECTION ( 'NONE',  ( 1.000000000000000000, 0.000000000000000000, 0.000000000000000000 ) ) ;
#10613=VERTEX_POINT ( 'NONE', #12243 ) ;
#10633=LINE ( 'NONE', #1019, #17582 ) ;
#10634=EDGE_CURVE ( 'NONE', #5440, #19306, #12678, .T. ) ;
#10642=DIRECTION ( 'NONE',  ( 1.000000000000000000, 0.000000000000000000, 0.000000000000000000 ) ) ;
#10658=DIRECTION ( 'NONE',  ( 0.000000000000000000, -1.000000000000000000, 0.000000000000000000 ) ) ;
#10691=ORIENTED_EDGE ( 'NONE', *, *, #15964, .T. ) ;
#10694=ORIENTED_EDGE ( 'NONE', *, *, #19971, .F. ) ;
#10732=DIRECTION ( 'NONE',  ( 0.000000000000000000, 1.000000000000000000, 0.000000000000000000 ) ) ;
#10738=ORIENTED_EDGE ( 'NONE', *, *, #2801, .F. ) ;
#10801=CARTESIAN_POINT ( 'NONE',  ( 5.569974746830579804, 0.000000000000000000, 0.000000000000000000 ) ) ;
#10803=ORIENTED_EDGE ( 'NONE', *, *, #17077, .T. ) ;
#10815=VERTEX_POINT ( 'NONE', #11732 ) ;
#10824=CYLINDRICAL_SURFACE ( 'NONE', #5965, 14.59999999999999964 ) ;
#10845=ORIENTED_EDGE ( 'NONE', *, *, #16596, .T. ) ;
#10848=SURFACE_STYLE_USAGE ( .BOTH. , #6127 ) ;
#10877=LINE ( 'NONE', #11085, #7337 ) ;
#10918=DIRECTION ( 'NONE',  ( 0.000000000000000000, 1.000000000000000000, 0.000000000000000000 ) ) ;
#10948=AXIS2_PLACEMENT_3D ( 'NONE', #5044, #10173, #17610 ) ;
#10955=( NAMED_UNIT ( * ) PLANE_ANGLE_UNIT ( ) SI_UNIT ( $, .RADIAN. ) );
#10981=DIRECTION ( 'NONE',  ( -1.000000000000000000, 0.000000000000000000, 0.000000000000000000 ) ) ;
#11018=DIRECTION ( 'NONE',  ( -1.000000000000000000, 0.000000000000000000, 0.000000000000000000 ) ) ;
#11042=FACE_OUTER_BOUND ( 'NONE', #16484, .T. ) ;
#11046=ADVANCED_FACE ( 'NONE', ( #8498 ), #295, .T. ) ;
#11051=FACE_OUTER_BOUND ( 'NONE', #12500, .T. ) ;
#11072=ORIENTED_EDGE ( 'NONE', *, *, #12400, .T. ) ;
#11078=CARTESIAN_POINT ( 'NONE',  ( 5.687501635565830327, 0.000000000000000000, 0.000000000000000000 ) ) ;
#11085=CARTESIAN_POINT ( 'NONE',  ( 3.324999999999999734, -12.97499999999999964, -1.588979221893690953E-15 ) ) ;
#11108=DIRECTION ( 'NONE',  ( 0.000000000000000000, 1.000000000000000000, 0.000000000000000000 ) ) ;
#11121=ORIENTED_EDGE ( 'NONE', *, *, #680, .F. ) ;
#11125=DIRECTION ( 'NONE',  ( 0.000000000000000000, 1.000000000000000000, 0.000000000000000000 ) ) ;
#11171=ORIENTED_EDGE ( 'NONE', *, *, #12382, .F. ) ;
#11212=CARTESIAN_POINT ( 'NONE',  ( 5.425003271131650706, 12.64814671169700055, 0.000000000000000000 ) ) ;
#11298=ORIENTED_EDGE ( 'NONE', *, *, #2427, .T. ) ;
#11315=DIRECTION ( 'NONE',  ( 0.6294249519366466039, -0.7770612780724246438, 9.516256069327462658E-17 ) ) ;
#11332=AXIS2_PLACEMENT_3D ( 'NONE', #19458, #11549, #706 ) ;
#11335=FACE_OUTER_BOUND ( 'NONE', #9810, .T. ) ;
#11350=EDGE_LOOP ( 'NONE', ( #17387, #18757, #16913, #3809 ) ) ;
#11358=CONICAL_SURFACE ( 'NONE', #2474, 13.62500000000000000, 0.2281026282799422378 ) ;
#11380=DIRECTION ( 'NONE',  ( -1.000000000000000000, 2.277380563333649802E-16, 0.000000000000000000 ) ) ;
#11405=ORIENTED_EDGE ( 'NONE', *, *, #17077, .F. ) ;
#11411=EDGE_CURVE ( 'NONE', #13085, #2774, #19478, .T. ) ;
#11431=CARTESIAN_POINT ( 'NONE',  ( 1.050000000000000044, 0.000000000000000000, 0.000000000000000000 ) ) ;
#11445=DIRECTION ( 'NONE',  ( 1.000000000000000000, 0.000000000000000000, 0.000000000000000000 ) ) ;
#11456=ORIENTED_EDGE ( 'NONE', *, *, #9470, .T. ) ;
#11468=CARTESIAN_POINT ( 'NONE',  ( -8.881784197001250351E-16, -17.85000000000000142, 2.225795557450314789E-15 ) ) ;
#11484=VERTEX_POINT ( 'NONE', #10325 ) ;
#11489=FACE_OUTER_BOUND ( 'NONE', #14988, .T. ) ;
#11504=ORIENTED_EDGE ( 'NONE', *, *, #15833, .F. ) ;
#11531=CIRCLE ( 'NONE', #6597, 14.27500000000000036 ) ;
#11549=DIRECTION ( 'NONE',  ( 1.000000000000000000, 0.000000000000000000, 0.000000000000000000 ) ) ;
#11565=CARTESIAN_POINT ( 'NONE',  ( 0.3499999999999999778, 0.000000000000000000, 0.000000000000000000 ) ) ;
#11568=CIRCLE ( 'NONE', #13217, 14.59999999999999964 ) ;
#11575=CARTESIAN_POINT ( 'NONE',  ( -8.881784197001250351E-16, 0.000000000000000000, 0.000000000000000000 ) ) ;
#11620=( LENGTH_UNIT ( ) NAMED_UNIT ( * ) SI_UNIT ( .MILLI., .METRE. ) );
#11646=CARTESIAN_POINT ( 'NONE',  ( 5.945602903476760126, 0.000000000000000000, 0.000000000000000000 ) ) ;
#11670=DIRECTION ( 'NONE',  ( 1.000000000000000000, 0.000000000000000000, 0.000000000000000000 ) ) ;
#11732=CARTESIAN_POINT ( 'NONE',  ( 6.299999999999999822, 18.50000000000000000, 0.000000000000000000 ) ) ;
#11735=AXIS2_PLACEMENT_3D ( 'NONE', #299, #4852, #6499 ) ;
#11736=( NAMED_UNIT ( * ) SI_UNIT ( $, .STERADIAN. ) SOLID_ANGLE_UNIT ( ) );
#11748=ORIENTED_EDGE ( 'NONE', *, *, #19325, .F. ) ;
#11755=DIRECTION ( 'NONE',  ( -0.7327934916262990317, 0.6804510993672779895, 0.000000000000000000 ) ) ;
#11760=CARTESIAN_POINT ( 'NONE',  ( 3.324999999999999734, 0.000000000000000000, 0.000000000000000000 ) ) ;
#11805=DIRECTION ( 'NONE',  ( 0.000000000000000000, 1.000000000000000000, 0.000000000000000000 ) ) ;
#11819=ORIENTED_EDGE ( 'NONE', *, *, #20138, .T. ) ;
#11831=DIRECTION ( 'NONE',  ( 0.000000000000000000, 1.000000000000000000, 0.000000000000000000 ) ) ;
#11854=DIRECTION ( 'NONE',  ( 0.000000000000000000, 1.000000000000000000, 0.000000000000000000 ) ) ;
#11856=LINE ( 'NONE', #7219, #4202 ) ;
#11889=CIRCLE ( 'NONE', #5627, 15.14120580695350071 ) ;
#11902=DIRECTION ( 'NONE',  ( -0.4740998230350218501, -0.8804710999221728729, -1.078266114261438272E-16 ) ) ;
#11954=CARTESIAN_POINT ( 'NONE',  ( 3.500000000000000000, 14.59999999999999964, 0.000000000000000000 ) ) ;
#12054=AXIS2_PLACEMENT_3D ( 'NONE', #6151, #15636, #12521 ) ;
#12079=CARTESIAN_POINT ( 'NONE',  ( 5.162501635565829972, 12.32407335584850117, 0.000000000000000000 ) ) ;
#12093=EDGE_CURVE ( 'NONE', #5629, #2165, #2663, .T. ) ;
#12114=ORIENTED_EDGE ( 'NONE', *, *, #6258, .F. ) ;
#12167=FACE_OUTER_BOUND ( 'NONE', #19639, .T. ) ;
#12169=FACE_OUTER_BOUND ( 'NONE', #4641, .T. ) ;
#12202=DIRECTION ( 'NONE',  ( 0.000000000000000000, 0.000000000000000000, -1.000000000000000000 ) ) ;
#12243=CARTESIAN_POINT ( 'NONE',  ( 5.950000000000000178, 12.65000000000000036, 0.000000000000000000 ) ) ;
#12360=( GEOMETRIC_REPRESENTATION_CONTEXT ( 3 ) GLOBAL_UNCERTAINTY_ASSIGNED_CONTEXT ( ( #19182 ) ) GLOBAL_UNIT_ASSIGNED_CONTEXT ( ( #20317, #10955, #1546 ) ) REPRESENTATION_CONTEXT ( 'NONE', 'WORKASPACE' ) );
#12382=EDGE_CURVE ( 'NONE', #18726, #15525, #9663, .T. ) ;
#12398=EDGE_CURVE ( 'NONE', #10613, #19303, #10576, .T. ) ;
#12400=EDGE_CURVE ( 'NONE', #2165, #10613, #10331, .T. ) ;
#12434=LINE ( 'NONE', #13764, #4288 ) ;
#12448=ORIENTED_EDGE ( 'NONE', *, *, #7392, .T. ) ;
#12500=EDGE_LOOP ( 'NONE', ( #16450, #1327, #14902, #1701 ) ) ;
#12521=DIRECTION ( 'NONE',  ( 0.000000000000000000, 1.000000000000000000, 0.000000000000000000 ) ) ;
#12533=ORIENTED_EDGE ( 'NONE', *, *, #680, .T. ) ;
#12536=CARTESIAN_POINT ( 'NONE',  ( 1.399999999999999911, 0.000000000000000000, 0.000000000000000000 ) ) ;
#12545=ORIENTED_EDGE ( 'NONE', *, *, #9427, .F. ) ;
#12561=DIRECTION ( 'NONE',  ( 0.000000000000000000, 1.000000000000000000, 0.000000000000000000 ) ) ;
#12573=VERTEX_POINT ( 'NONE', #8206 ) ;
#12578=CYLINDRICAL_SURFACE ( 'NONE', #6129, 18.50000000000000000 ) ;
#12580=CARTESIAN_POINT ( 'NONE',  ( 5.687501635565830327, 12.64907335584850046, 0.000000000000000000 ) ) ;
#12605=CARTESIAN_POINT ( 'NONE',  ( 5.044974746830580337, 0.000000000000000000, -14.76997474683059153 ) ) ;
#12620=AXIS2_PLACEMENT_3D ( 'NONE', #1193, #7521, #4320 ) ;
#12621=ORIENTED_EDGE ( 'NONE', *, *, #9123, .F. ) ;
#12669=CIRCLE ( 'NONE', #11332, 13.95000000000000107 ) ;
#12678=CIRCLE ( 'NONE', #17616, 14.27500000000000036 ) ;
#12705=CARTESIAN_POINT ( 'NONE',  ( 1.224999999999999867, -15.25000000000000000, -1.867586368699713770E-15 ) ) ;
#12720=TOROIDAL_SURFACE ( 'NONE', #9408, 14.27500000000000036, 0.6999999999999999556 ) ;
#12738=ORIENTED_EDGE ( 'NONE', *, *, #9718, .F. ) ;
#12744=DIRECTION ( 'NONE',  ( 0.000000000000000000, 1.000000000000000000, 0.000000000000000000 ) ) ;
#12746=CARTESIAN_POINT ( 'NONE',  ( 5.569974746830579804, 0.000000000000000000, -14.76997474683060041 ) ) ;
#12751=ORIENTED_EDGE ( 'NONE', *, *, #1919, .F. ) ;
#12759=CARTESIAN_POINT ( 'NONE',  ( 5.569974746830579804, 1.808800229719333629E-15, 14.76997474683060041 ) ) ;
#12765=DIRECTION ( 'NONE',  ( 1.000000000000000000, 0.000000000000000000, 0.000000000000000000 ) ) ;
#12788=EDGE_LOOP ( 'NONE', ( #4846, #8703 ) ) ;
#12837=DIRECTION ( 'NONE',  ( 0.000000000000000000, 1.000000000000000000, 0.000000000000000000 ) ) ;
#12845=AXIS2_PLACEMENT_3D ( 'NONE', #12759, #13877, #15657 ) ;
#12863=ORIENTED_EDGE ( 'NONE', *, *, #16427, .F. ) ;
#12874=ORIENTED_EDGE ( 'NONE', *, *, #2694, .T. ) ;
#12878=CARTESIAN_POINT ( 'NONE',  ( 5.044974746830580337, 1.808800229719332446E-15, 14.76997474683059153 ) ) ;
#12888=ORIENTED_EDGE ( 'NONE', *, *, #18797, .T. ) ;
#12938=FACE_BOUND ( 'NONE', #482, .T. ) ;
#12948=DIRECTION ( 'NONE',  ( 1.000000000000000000, 0.000000000000000000, 0.000000000000000000 ) ) ;
#12961=ORIENTED_EDGE ( 'NONE', *, *, #9139, .F. ) ;
#12971=CIRCLE ( 'NONE', #765, 15.25000000000000000 ) ;
#13017=DIRECTION ( 'NONE',  ( 1.000000000000000000, 0.000000000000000000, 0.000000000000000000 ) ) ;
#13055=ADVANCED_FACE ( 'NONE', ( #4045 ), #11358, .F. ) ;
#13085=VERTEX_POINT ( 'NONE', #17956 ) ;
#13086=CIRCLE ( 'NONE', #17331, 13.29999999999999893 ) ;
#13115=FACE_OUTER_BOUND ( 'NONE', #9606, .T. ) ;
#13118=AXIS2_PLACEMENT_3D ( 'NONE', #14528, #14641, #6508 ) ;
#13128=ORIENTED_EDGE ( 'NONE', *, *, #13658, .T. ) ;
#13136=DIRECTION ( 'NONE',  ( -0.8502651466878615727, 0.5263546146162958461, 0.000000000000000000 ) ) ;
#13143=ORIENTED_EDGE ( 'NONE', *, *, #12400, .F. ) ;
#13152=ORIENTED_EDGE ( 'NONE', *, *, #5992, .T. ) ;
#13187=DIRECTION ( 'NONE',  ( 1.000000000000000000, 0.000000000000000000, 0.000000000000000000 ) ) ;
#13195=CIRCLE ( 'NONE', #4287, 18.50000000000000000 ) ;
#13215=CARTESIAN_POINT ( 'NONE',  ( 0.6999999999999999556, -18.50000000000000000, -2.265596578422603396E-15 ) ) ;
#13217=AXIS2_PLACEMENT_3D ( 'NONE', #18427, #10603, #4234 ) ;
#13223=EDGE_LOOP ( 'NONE', ( #17177, #12961, #3810, #14930 ) ) ;
#13235=CARTESIAN_POINT ( 'NONE',  ( 1.050000000000000044, 17.52499999999999858, 0.000000000000000000 ) ) ;
#13291=DIRECTION ( 'NONE',  ( 0.000000000000000000, 1.000000000000000000, 0.000000000000000000 ) ) ;
#13316=FACE_OUTER_BOUND ( 'NONE', #1156, .T. ) ;
#13325=CARTESIAN_POINT ( 'NONE',  ( 3.674999999999999822, -14.43750000000000000, -1.768083816268991068E-15 ) ) ;
#13365=COLOUR_RGB ( '', 0.31764706, 0.68627451, 0.89019608) ;
#13381=CIRCLE ( 'NONE', #4473, 17.52499999999999858 ) ;
#13406=ADVANCED_FACE ( 'NONE', ( #3898 ), #1041, .T. ) ;
#13421=EDGE_CURVE ( 'NONE', #15933, #5629, #8446, .T. ) ;
#13427=ORIENTED_EDGE ( 'NONE', *, *, #8291, .T. ) ;
#13506=AXIS2_PLACEMENT_3D ( 'NONE', #487, #17481, #11108 ) ;
#13522=DIRECTION ( 'NONE',  ( -1.000000000000000000, 0.000000000000000000, 0.000000000000000000 ) ) ;
#13540=AXIS2_PLACEMENT_3D ( 'NONE', #18953, #15698, #20372 ) ;
#13571=DIRECTION ( 'NONE',  ( 0.000000000000000000, 1.000000000000000000, 0.000000000000000000 ) ) ;
#13588=AXIS2_PLACEMENT_3D ( 'NONE', #15744, #15533, #14166 ) ;
#13606=CIRCLE ( 'NONE', #13928, 18.50000000000000000 ) ;
#13610=VERTEX_POINT ( 'NONE', #14180 ) ;
#13618=DIRECTION ( 'NONE',  ( 1.000000000000000000, 0.000000000000000000, 0.000000000000000000 ) ) ;
#13637=AXIS2_PLACEMENT_3D ( 'NONE', #16875, #18193, #11831 ) ;
#13648=CARTESIAN_POINT ( 'NONE',  ( 6.649999999999999467, -18.17500000000000071, -2.225795557450314789E-15 ) ) ;
#13654=CARTESIAN_POINT ( 'NONE',  ( 6.299999999999999822, 0.000000000000000000, 0.000000000000000000 ) ) ;
#13658=EDGE_CURVE ( 'NONE', #15899, #15076, #17211, .T. ) ;
#13668=ADVANCED_FACE ( 'NONE', ( #19005 ), #5047, .T. ) ;
#13676=EDGE_CURVE ( 'NONE', #8577, #18077, #15904, .T. ) ;
#13690=ORIENTED_EDGE ( 'NONE', *, *, #16216, .T. ) ;
#13758=ORIENTED_EDGE ( 'NONE', *, *, #3811, .F. ) ;
#13764=CARTESIAN_POINT ( 'NONE',  ( 2.625000000000000000, 14.59999999999999964, 0.000000000000000000 ) ) ;
#13791=DIRECTION ( 'NONE',  ( 0.9999937692730440641, -0.003530072958125829961, 4.323092548925426475E-19 ) ) ;
#13812=DIRECTION ( 'NONE',  ( 0.000000000000000000, 1.000000000000000000, 0.000000000000000000 ) ) ;
#13835=ORIENTED_EDGE ( 'NONE', *, *, #18821, .F. ) ;
#13877=DIRECTION ( 'NONE',  ( 0.000000000000000000, 1.000000000000000000, -1.224646799147353207E-16 ) ) ;
#13905=PRODUCT_DEFINITION_FORMATION_WITH_SPECIFIED_SOURCE ( 'ANY', '', #15518, .NOT_KNOWN. ) ;
#13919=EDGE_CURVE ( 'NONE', #10613, #2165, #18204, .T. ) ;
#13928=AXIS2_PLACEMENT_3D ( 'NONE', #15144, #20063, #18732 ) ;
#13947=ADVANCED_FACE ( 'NONE', ( #18039 ), #10216, .T. ) ;
#13953=VERTEX_POINT ( 'NONE', #7151 ) ;
#13970=VECTOR ( 'NONE', #1745, 1000.000000000000000 ) ;
#14000=ORIENTED_EDGE ( 'NONE', *, *, #17159, .F. ) ;
#14029=DIRECTION ( 'NONE',  ( 1.000000000000000000, 0.000000000000000000, 0.000000000000000000 ) ) ;
#14038=ADVANCED_FACE ( 'NONE', ( #1424 ), #14221, .F. ) ;
#14053=EDGE_CURVE ( 'NONE', #5220, #10613, #9392, .T. ) ;
#14059=FACE_OUTER_BOUND ( 'NONE', #20362, .T. ) ;
#14129=ORIENTED_EDGE ( 'NONE', *, *, #7283, .T. ) ;
#14166=DIRECTION ( 'NONE',  ( 0.000000000000000000, 1.224646799147356165E-16, 1.000000000000000000 ) ) ;
#14167=DIRECTION ( 'NONE',  ( 0.000000000000000000, -1.000000000000000000, 0.000000000000000000 ) ) ;
#14180=CARTESIAN_POINT ( 'NONE',  ( 1.050000000000000044, -17.52499999999999858, -2.146193515505736390E-15 ) ) ;
#14184=CIRCLE ( 'NONE', #1303, 15.14120580695350071 ) ;
#14218=CARTESIAN_POINT ( 'NONE',  ( 1.050000000000000044, 0.000000000000000000, 0.000000000000000000 ) ) ;
#14221=CYLINDRICAL_SURFACE ( 'NONE', #8354, 17.52499999999999858 ) ;
#14235=AXIS2_PLACEMENT_3D ( 'NONE', #6167, #57, #3166 ) ;
#14257=ORIENTED_EDGE ( 'NONE', *, *, #13676, .T. ) ;
#14270=DIRECTION ( 'NONE',  ( 0.000000000000000000, 1.000000000000000000, 0.000000000000000000 ) ) ;
#14318=EDGE_CURVE ( 'NONE', #15933, #13085, #18601, .T. ) ;
#14325=AXIS2_PLACEMENT_3D ( 'NONE', #20344, #4810, #14270 ) ;
#14332=DIRECTION ( 'NONE',  ( 0.000000000000000000, 1.000000000000000000, 0.000000000000000000 ) ) ;
#14349=CARTESIAN_POINT ( 'NONE',  ( 5.044974746830580337, 0.000000000000000000, 0.000000000000000000 ) ) ;
#14368=PLANE ( 'NONE',  #20125 ) ;
#14372=ORIENTED_EDGE ( 'NONE', *, *, #19971, .T. ) ;
#14421=ORIENTED_EDGE ( 'NONE', *, *, #19351, .T. ) ;
#14429=ADVANCED_FACE ( 'NONE', ( #6667 ), #1453, .T. ) ;
#14474=DIRECTION ( 'NONE',  ( 0.000000000000000000, 1.000000000000000000, 0.000000000000000000 ) ) ;
#14526=DIRECTION ( 'NONE',  ( 0.000000000000000000, 1.000000000000000000, 0.000000000000000000 ) ) ;
#14528=CARTESIAN_POINT ( 'NONE',  ( 1.574999999999999956, 0.000000000000000000, 0.000000000000000000 ) ) ;
#14533=CARTESIAN_POINT ( 'NONE',  ( 4.899999999999999467, -12.00000000000000000, 1.509263698769704680E-15 ) ) ;
#14544=ADVANCED_FACE ( 'NONE', ( #11489 ), #16968, .T. ) ;
#14560=CARTESIAN_POINT ( 'NONE',  ( -1.776356839400249676E-15, 15.90000000000000036, 0.000000000000000000 ) ) ;
#14574=CYLINDRICAL_SURFACE ( 'NONE', #15802, 15.25000000000000000 ) ;
#14593=EDGE_LOOP ( 'NONE', ( #9208, #19087 ) ) ;
#14641=DIRECTION ( 'NONE',  ( -1.000000000000000000, 0.000000000000000000, 0.000000000000000000 ) ) ;
#14650=CIRCLE ( 'NONE', #4134, 17.85000000000000142 ) ;
#14674=DIRECTION ( 'NONE',  ( 1.000000000000000000, 0.000000000000000000, 0.000000000000000000 ) ) ;
#14681=ORIENTED_EDGE ( 'NONE', *, *, #4335, .T. ) ;
#14683=CARTESIAN_POINT ( 'NONE',  ( 2.799999999999999822, -13.30000000000000071, -1.628780242865979955E-15 ) ) ;
#14700=DIRECTION ( 'NONE',  ( -1.000000000000000000, 0.000000000000000000, 0.000000000000000000 ) ) ;
#14728=ORIENTED_EDGE ( 'NONE', *, *, #11411, .T. ) ;
#14738=CARTESIAN_POINT ( 'NONE',  ( 2.799999999999999822, 0.000000000000000000, 0.000000000000000000 ) ) ;
#14743=EDGE_CURVE ( 'NONE', #18280, #17493, #16756, .T. ) ;
#14804=CARTESIAN_POINT ( 'NONE',  ( -1.776356839400249676E-15, 13.94999999999999929, 0.000000000000000000 ) ) ;
#14816=VERTEX_POINT ( 'NONE', #5494 ) ;
#14835=FACE_OUTER_BOUND ( 'NONE', #18788, .T. ) ;
#14848=LINE ( 'NONE', #13325, #7087 ) ;
#14874=ORIENTED_EDGE ( 'NONE', *, *, #18821, .T. ) ;
#14896=CIRCLE ( 'NONE', #13588, 0.6999999999999992895 ) ;
#14902=ORIENTED_EDGE ( 'NONE', *, *, #19290, .T. ) ;
#14904=VERTEX_POINT ( 'NONE', #8792 ) ;
#14929=VECTOR ( 'NONE', #20298, 1000.000000000000227 ) ;
#14930=ORIENTED_EDGE ( 'NONE', *, *, #13919, .T. ) ;
#14950=DIRECTION ( 'NONE',  ( 0.000000000000000000, 1.000000000000000000, 0.000000000000000000 ) ) ;
#14988=EDGE_LOOP ( 'NONE', ( #8039, #4889, #289, #5924 ) ) ;
#15057=DIRECTION ( 'NONE',  ( -0.7327934916262990317, -0.6804510993672779895, -8.333122608164345406E-17 ) ) ;
#15064=DIRECTION ( 'NONE',  ( -1.000000000000000000, 0.000000000000000000, 0.000000000000000000 ) ) ;
#15076=VERTEX_POINT ( 'NONE', #518 ) ;
#15079=DIRECTION ( 'NONE',  ( -0.9740972002433518906, 0.2261297071993489949, 0.000000000000000000 ) ) ;
#15106=EDGE_LOOP ( 'NONE', ( #7418, #17353, #12533, #12888 ) ) ;
#15144=CARTESIAN_POINT ( 'NONE',  ( 6.299999999999999822, 0.000000000000000000, 0.000000000000000000 ) ) ;
#15149=EDGE_CURVE ( 'NONE', #12573, #8577, #5605, .T. ) ;
#15161=EDGE_CURVE ( 'NONE', #10815, #11484, #10350, .T. ) ;
#15197=ORIENTED_EDGE ( 'NONE', *, *, #5960, .F. ) ;
#15199=CARTESIAN_POINT ( 'NONE',  ( 4.549999999999999822, 0.000000000000000000, -14.27500000000000036 ) ) ;
#15234=AXIS2_PLACEMENT_3D ( 'NONE', #7698, #15435, #20146 ) ;
#15248=DIRECTION ( 'NONE',  ( 1.000000000000000000, 0.000000000000000000, 0.000000000000000000 ) ) ;
#15264=AXIS2_PLACEMENT_3D ( 'NONE', #6301, #9572, #14332 ) ;
#15266=DIRECTION ( 'NONE',  ( -1.000000000000000000, 0.000000000000000000, 0.000000000000000000 ) ) ;
#15352=CIRCLE ( 'NONE', #9094, 17.52499999999999858 ) ;
#15354=FACE_OUTER_BOUND ( 'NONE', #10282, .T. ) ;
#15386=ORIENTED_EDGE ( 'NONE', *, *, #12398, .F. ) ;
#15398=CARTESIAN_POINT ( 'NONE',  ( 1.574999999999999956, -14.92500000000000071, -1.827785347727424768E-15 ) ) ;
#15414=ORIENTED_EDGE ( 'NONE', *, *, #4335, .F. ) ;
#15435=DIRECTION ( 'NONE',  ( 1.000000000000000000, 0.000000000000000000, 0.000000000000000000 ) ) ;
#15449=CARTESIAN_POINT ( 'NONE',  ( 1.574999999999999956, 14.92500000000000071, 0.000000000000000000 ) ) ;
#15518=PRODUCT ( '722909', '722909', '', ( #3017 ) ) ;
#15525=VERTEX_POINT ( 'NONE', #16987 ) ;
#15533=DIRECTION ( 'NONE',  ( 0.000000000000000000, 1.000000000000000000, -1.224646799147353207E-16 ) ) ;
#15534=APPLICATION_CONTEXT ( 'automotive_design' ) ;
#15551=ORIENTED_EDGE ( 'NONE', *, *, #1919, .T. ) ;
#15622=VERTEX_POINT ( 'NONE', #13235 ) ;
#15636=DIRECTION ( 'NONE',  ( 1.000000000000000000, 0.000000000000000000, 0.000000000000000000 ) ) ;
#15653=CARTESIAN_POINT ( 'NONE',  ( 3.850000000000000089, -14.27500000000000036, -1.768083816268991068E-15 ) ) ;
#15657=DIRECTION ( 'NONE',  ( 0.000000000000000000, 1.224646799147356165E-16, 1.000000000000000000 ) ) ;
#15698=DIRECTION ( 'NONE',  ( 1.000000000000000000, 0.000000000000000000, 0.000000000000000000 ) ) ;
#15744=CARTESIAN_POINT ( 'NONE',  ( 4.549999999999999822, 1.748183305782846567E-15, 14.27500000000000036 ) ) ;
#15781=ORIENTED_EDGE ( 'NONE', *, *, #7791, .T. ) ;
#15798=DIRECTION ( 'NONE',  ( -1.000000000000000000, 0.000000000000000000, 0.000000000000000000 ) ) ;
#15802=AXIS2_PLACEMENT_3D ( 'NONE', #6663, #8202, #14474 ) ;
#15803=DIRECTION ( 'NONE',  ( -1.000000000000000000, 0.000000000000000000, 0.000000000000000000 ) ) ;
#15833=EDGE_CURVE ( 'NONE', #8577, #8093, #16021, .T. ) ;
#15842=DIRECTION ( 'NONE',  ( -0.8502651466878615727, -0.5263546146162958461, -6.445984940062853155E-17 ) ) ;
#15847=ORIENTED_EDGE ( 'NONE', *, *, #20138, .F. ) ;
#15899=VERTEX_POINT ( 'NONE', #409 ) ;
#15901=LINE ( 'NONE', #6422, #8722 ) ;
#15904=CIRCLE ( 'NONE', #15234, 15.25000000000000000 ) ;
#15929=ORIENTED_EDGE ( 'NONE', *, *, #18797, .F. ) ;
#15932=ORIENTED_EDGE ( 'NONE', *, *, #13919, .F. ) ;
#15933=VERTEX_POINT ( 'NONE', #14533 ) ;
#15934=ADVANCED_FACE ( 'NONE', ( #13316 ), #18896, .F. ) ;
#15935=CONICAL_SURFACE ( 'NONE', #4720, 14.43750000000000000, 0.7483780475235185525 ) ;
#15937=DIRECTION ( 'NONE',  ( 1.000000000000000000, 0.000000000000000000, 0.000000000000000000 ) ) ;
#15964=EDGE_CURVE ( 'NONE', #14816, #8147, #12669, .T. ) ;
#15972=EDGE_LOOP ( 'NONE', ( #11504, #15929, #10309, #13690 ) ) ;
#16021=LINE ( 'NONE', #12705, #13970 ) ;
#16057=ORIENTED_EDGE ( 'NONE', *, *, #9483, .T. ) ;
#16076=ORIENTED_EDGE ( 'NONE', *, *, #7475, .F. ) ;
#16137=CARTESIAN_POINT ( 'NONE',  ( 5.941205806953520074, 0.000000000000000000, 0.000000000000000000 ) ) ;
#16138=DIRECTION ( 'NONE',  ( 1.000000000000000000, 0.000000000000000000, 0.000000000000000000 ) ) ;
#16148=DIRECTION ( 'NONE',  ( 0.6294249519366466039, 0.7770612780724246438, 0.000000000000000000 ) ) ;
#16174=AXIS2_PLACEMENT_3D ( 'NONE', #1671, #16793, #6453 ) ;
#16216=EDGE_CURVE ( 'NONE', #1892, #8093, #3270, .T. ) ;
#16218=FACE_OUTER_BOUND ( 'NONE', #16887, .T. ) ;
#16288=CIRCLE ( 'NONE', #6075, 17.85000000000000142 ) ;
#16305=CONICAL_SURFACE ( 'NONE', #3779, 13.62500000000000000, 0.2281026282799422378 ) ;
#16309=DIRECTION ( 'NONE',  ( 1.000000000000000000, 0.000000000000000000, 0.000000000000000000 ) ) ;
#16330=VECTOR ( 'NONE', #16148, 1000.000000000000000 ) ;
#16409=CIRCLE ( 'NONE', #5527, 18.50000000000000000 ) ;
#16419=ORIENTED_EDGE ( 'NONE', *, *, #15161, .T. ) ;
#16421=DIRECTION ( 'NONE',  ( 1.000000000000000000, 0.000000000000000000, 0.000000000000000000 ) ) ;
#16427=EDGE_CURVE ( 'NONE', #4190, #15899, #958, .T. ) ;
#16434=DIRECTION ( 'NONE',  ( 0.000000000000000000, 1.000000000000000000, 0.000000000000000000 ) ) ;
#16450=ORIENTED_EDGE ( 'NONE', *, *, #9470, .F. ) ;
#16484=EDGE_LOOP ( 'NONE', ( #1767, #5526, #2086, #4023, #1130 ) ) ;
#16498=AXIS2_PLACEMENT_3D ( 'NONE', #11431, #7003, #13291 ) ;
#16503=DIRECTION ( 'NONE',  ( -1.000000000000000000, 0.000000000000000000, 0.000000000000000000 ) ) ;
#16521=CARTESIAN_POINT ( 'NONE',  ( -1.776356839400249676E-15, 0.000000000000000000, 0.000000000000000000 ) ) ;
#16524=CARTESIAN_POINT ( 'NONE',  ( 3.500000000000000000, 0.000000000000000000, 0.000000000000000000 ) ) ;
#16596=EDGE_CURVE ( 'NONE', #8554, #6498, #17439, .T. ) ;
#16631=CARTESIAN_POINT ( 'NONE',  ( 3.500000000000000000, -18.50000000000000000, -2.265596578422603396E-15 ) ) ;
#16643=DIRECTION ( 'NONE',  ( 0.000000000000000000, 1.000000000000000000, 0.000000000000000000 ) ) ;
#16662=CARTESIAN_POINT ( 'NONE',  ( 3.500000000000000000, 18.50000000000000000, 0.000000000000000000 ) ) ;
#16704=ORIENTED_EDGE ( 'NONE', *, *, #6881, .T. ) ;
#16719=EDGE_CURVE ( 'NONE', #10815, #17493, #13195, .T. ) ;
#16720=CARTESIAN_POINT ( 'NONE',  ( 5.941205806953520074, 0.000000000000000000, -15.14120580695351670 ) ) ;
#16739=CARTESIAN_POINT ( 'NONE',  ( 1.399999999999999911, 0.000000000000000000, 0.000000000000000000 ) ) ;
#16756=LINE ( 'NONE', #13648, #6447 ) ;
#16793=DIRECTION ( 'NONE',  ( 1.000000000000000000, -6.123031769111888756E-17, 0.000000000000000000 ) ) ;
#16804=CIRCLE ( 'NONE', #1625, 17.85000000000000142 ) ;
#16840=DIRECTION ( 'NONE',  ( 0.000000000000000000, 1.000000000000000000, 0.000000000000000000 ) ) ;
#16849=ORIENTED_EDGE ( 'NONE', *, *, #16719, .F. ) ;
#16875=CARTESIAN_POINT ( 'NONE',  ( 5.950000000000000178, 0.000000000000000000, 0.000000000000000000 ) ) ;
#16887=EDGE_LOOP ( 'NONE', ( #19597, #2422 ) ) ;
#16907=AXIS2_PLACEMENT_3D ( 'NONE', #5173, #11445, #17723 ) ;
#16913=ORIENTED_EDGE ( 'NONE', *, *, #187, .T. ) ;
#16921=CARTESIAN_POINT ( 'NONE',  ( 5.162501635565829972, 0.000000000000000000, 0.000000000000000000 ) ) ;
#16968=CONICAL_SURFACE ( 'NONE', #8074, 18.17500000000000071, 0.7483780475235185525 ) ;
#16971=FACE_OUTER_BOUND ( 'NONE', #13223, .T. ) ;
#16987=CARTESIAN_POINT ( 'NONE',  ( 3.850000000000000089, 0.000000000000000000, -14.27500000000000036 ) ) ;
#17037=ORIENTED_EDGE ( 'NONE', *, *, #2427, .F. ) ;
#17077=EDGE_CURVE ( 'NONE', #15076, #19612, #14184, .T. ) ;
#17082=DIRECTION ( 'NONE',  ( 1.000000000000000000, 0.000000000000000000, 0.000000000000000000 ) ) ;
#17128=PRESENTATION_STYLE_ASSIGNMENT (( #10848 ) ) ;
#17159=EDGE_CURVE ( 'NONE', #6498, #8554, #11568, .T. ) ;
#17170=ORIENTED_EDGE ( 'NONE', *, *, #17159, .T. ) ;
#17177=ORIENTED_EDGE ( 'NONE', *, *, #12093, .F. ) ;
#17211=CIRCLE ( 'NONE', #19823, 15.14120580695350071 ) ;
#17223=DIRECTION ( 'NONE',  ( -1.000000000000000000, 0.000000000000000000, 0.000000000000000000 ) ) ;
#17230=DIRECTION ( 'NONE',  ( 1.000000000000000000, 0.000000000000000000, 0.000000000000000000 ) ) ;
#17276=DIRECTION ( 'NONE',  ( 1.000000000000000000, 0.000000000000000000, 0.000000000000000000 ) ) ;
#17300=AXIS2_PLACEMENT_3D ( 'NONE', #2829, #20128, #12837 ) ;
#17315=LINE ( 'NONE', #19151, #203 ) ;
#17330=CARTESIAN_POINT ( 'NONE',  ( 1.399999999999999911, 0.000000000000000000, 0.000000000000000000 ) ) ;
#17331=AXIS2_PLACEMENT_3D ( 'NONE', #9861, #12765, #8013 ) ;
#17338=DIRECTION ( 'NONE',  ( 0.000000000000000000, 1.000000000000000000, 0.000000000000000000 ) ) ;
#17353=ORIENTED_EDGE ( 'NONE', *, *, #68, .F. ) ;
#17387=ORIENTED_EDGE ( 'NONE', *, *, #13676, .F. ) ;
#17439=CIRCLE ( 'NONE', #9892, 14.59999999999999964 ) ;
#17455=VECTOR ( 'NONE', #5496, 1000.000000000000000 ) ;
#17481=DIRECTION ( 'NONE',  ( 1.000000000000000000, 0.000000000000000000, 0.000000000000000000 ) ) ;
#17493=VERTEX_POINT ( 'NONE', #10392 ) ;
#17501=AXIS2_PLACEMENT_3D ( 'NONE', #2634, #7494, #7584 ) ;
#17502=CARTESIAN_POINT ( 'NONE',  ( 7.000000000000000000, -17.52499999999999858, -2.146193515505736390E-15 ) ) ;
#17518=VECTOR ( 'NONE', #13136, 1000.000000000000114 ) ;
#17541=DIRECTION ( 'NONE',  ( -1.000000000000000000, 0.000000000000000000, 0.000000000000000000 ) ) ;
#17544=AXIS2_PLACEMENT_3D ( 'NONE', #16524, #13522, #837 ) ;
#17557=AXIS2_PLACEMENT_3D ( 'NONE', #5446, #4295, #13571 ) ;
#17572=CARTESIAN_POINT ( 'NONE',  ( 4.025000000000000355, 0.000000000000000000, 0.000000000000000000 ) ) ;
#17582=VECTOR ( 'NONE', #15079, 1000.000000000000114 ) ;
#17610=DIRECTION ( 'NONE',  ( 0.000000000000000000, 1.000000000000000000, 0.000000000000000000 ) ) ;
#17616=AXIS2_PLACEMENT_3D ( 'NONE', #18521, #15248, #4418 ) ;
#17629=DIRECTION ( 'NONE',  ( 0.000000000000000000, 0.000000000000000000, -1.000000000000000000 ) ) ;
#17655=FACE_OUTER_BOUND ( 'NONE', #19059, .T. ) ;
#17712=EDGE_LOOP ( 'NONE', ( #12863, #15781, #3703, #11405, #1074 ) ) ;
#17722=DIRECTION ( 'NONE',  ( 0.000000000000000000, 1.000000000000000000, 0.000000000000000000 ) ) ;
#17723=DIRECTION ( 'NONE',  ( 0.000000000000000000, 1.000000000000000000, 0.000000000000000000 ) ) ;
#17746=CIRCLE ( 'NONE', #1290, 17.52499999999999858 ) ;
#17792=EDGE_CURVE ( 'NONE', #15525, #19679, #3362, .T. ) ;
#17817=CARTESIAN_POINT ( 'NONE',  ( 2.799999999999999822, 13.30000000000000071, 0.000000000000000000 ) ) ;
#17819=DIRECTION ( 'NONE',  ( -1.000000000000000000, 0.000000000000000000, 0.000000000000000000 ) ) ;
#17880=CONICAL_SURFACE ( 'NONE', #8990, 13.89560290347679938, 1.567266246505109928 ) ;
#17948=DIRECTION ( 'NONE',  ( 0.000000000000000000, 1.000000000000000000, 0.000000000000000000 ) ) ;
#17956=CARTESIAN_POINT ( 'NONE',  ( 4.899999999999999467, 12.00000000000000000, 0.000000000000000000 ) ) ;
#17987=ORIENTED_EDGE ( 'NONE', *, *, #19325, .T. ) ;
#18002=CARTESIAN_POINT ( 'NONE',  ( 3.850000000000000089, 14.27500000000000036, 0.000000000000000000 ) ) ;
#18013=ORIENTED_EDGE ( 'NONE', *, *, #14318, .F. ) ;
#18026=ADVANCED_FACE ( 'NONE', ( #12938, #3448 ), #14368, .T. ) ;
#18039=FACE_OUTER_BOUND ( 'NONE', #2006, .T. ) ;
#18043=DIRECTION ( 'NONE',  ( -1.000000000000000000, 0.000000000000000000, 0.000000000000000000 ) ) ;
#18077=VERTEX_POINT ( 'NONE', #5941 ) ;
#18103=PRODUCT_DEFINITION_CONTEXT ( 'detailed design', #5268, 'design' ) ;
#18140=CARTESIAN_POINT ( 'NONE',  ( 0.3499999999999999778, -18.17500000000000071, 2.225795557450314789E-15 ) ) ;
#18175=ORIENTED_EDGE ( 'NONE', *, *, #7283, .F. ) ;
#18193=DIRECTION ( 'NONE',  ( 1.000000000000000000, 0.000000000000000000, 0.000000000000000000 ) ) ;
#18204=CIRCLE ( 'NONE', #3069, 12.65000000000000036 ) ;
#18272=LINE ( 'NONE', #4061, #2618 ) ;
#18274=STYLED_ITEM ( 'NONE', ( #17128 ), #2209 ) ;
#18280=VERTEX_POINT ( 'NONE', #570 ) ;
#18346=DIRECTION ( 'NONE',  ( 0.000000000000000000, 1.000000000000000000, 0.000000000000000000 ) ) ;
#18371=ORIENTED_EDGE ( 'NONE', *, *, #9427, .T. ) ;
#18427=CARTESIAN_POINT ( 'NONE',  ( 3.500000000000000000, 0.000000000000000000, 0.000000000000000000 ) ) ;
#18521=CARTESIAN_POINT ( 'NONE',  ( 3.850000000000000089, 0.000000000000000000, 0.000000000000000000 ) ) ;
#18533=ORIENTED_EDGE ( 'NONE', *, *, #6922, .T. ) ;
#18572=VECTOR ( 'NONE', #6212, 1000.000000000000000 ) ;
#18582=AXIS2_PLACEMENT_3D ( 'NONE', #19464, #8064, #5379 ) ;
#18601=CIRCLE ( 'NONE', #4127, 12.00000000000000000 ) ;
#18609=LINE ( 'NONE', #2735, #4 ) ;
#18619=DIRECTION ( 'NONE',  ( 1.000000000000000000, 0.000000000000000000, 0.000000000000000000 ) ) ;
#18620=CONICAL_SURFACE ( 'NONE', #5151, 18.17500000000000071, 0.7483780475235185525 ) ;
#18632=AXIS2_PLACEMENT_3D ( 'NONE', #807, #16309, #5557 ) ;
#18633=DIRECTION ( 'NONE',  ( -0.4740998230350218501, 0.8804710999221728729, 0.000000000000000000 ) ) ;
#18637=CIRCLE ( 'NONE', #11735, 12.64814671169700055 ) ;
#18673=CARTESIAN_POINT ( 'NONE',  ( 5.941205806953520074, 0.000000000000000000, 0.000000000000000000 ) ) ;
#18682=EDGE_LOOP ( 'NONE', ( #10694, #5422, #17987, #2025 ) ) ;
#18726=VERTEX_POINT ( 'NONE', #15653 ) ;
#18732=DIRECTION ( 'NONE',  ( 0.000000000000000000, 1.000000000000000000, 0.000000000000000000 ) ) ;
#18734=ORIENTED_EDGE ( 'NONE', *, *, #8328, .T. ) ;
#18757=ORIENTED_EDGE ( 'NONE', *, *, #15833, .T. ) ;
#18770=CARTESIAN_POINT ( 'NONE',  ( 5.950000000000000178, -12.65000000000000036, -1.701720561796546765E-15 ) ) ;
#18788=EDGE_LOOP ( 'NONE', ( #13143, #16704, #10803, #20273, #15386 ) ) ;
#18797=EDGE_CURVE ( 'NONE', #18077, #8577, #12971, .T. ) ;
#18818=ORIENTED_EDGE ( 'NONE', *, *, #9011, .T. ) ;
#18821=EDGE_CURVE ( 'NONE', #8554, #12573, #9755, .T. ) ;
#18838=EDGE_LOOP ( 'NONE', ( #20249, #15932, #9704, #12448, #13128 ) ) ;
#18857=LINE ( 'NONE', #7948, #18572 ) ;
#18896=CONICAL_SURFACE ( 'NONE', #8389, 12.32407335584850117, 0.8899833664651138898 ) ;
#18906=DIRECTION ( 'NONE',  ( 1.000000000000000000, 0.000000000000000000, 0.000000000000000000 ) ) ;
#18953=CARTESIAN_POINT ( 'NONE',  ( 4.899999999999999467, 0.000000000000000000, 0.000000000000000000 ) ) ;
#18955=DIRECTION ( 'NONE',  ( -1.000000000000000000, 0.000000000000000000, 0.000000000000000000 ) ) ;
#18966=ORIENTED_EDGE ( 'NONE', *, *, #16427, .T. ) ;
#19005=FACE_OUTER_BOUND ( 'NONE', #19502, .T. ) ;
#19035=AXIS2_PLACEMENT_3D ( 'NONE', #8418, #5515, #11805 ) ;
#19059=EDGE_LOOP ( 'NONE', ( #8321, #2047, #14728, #333 ) ) ;
#19087=ORIENTED_EDGE ( 'NONE', *, *, #19187, .F. ) ;
#19096=CARTESIAN_POINT ( 'NONE',  ( 1.050000000000000044, 0.000000000000000000, 0.000000000000000000 ) ) ;
#19122=ORIENTED_EDGE ( 'NONE', *, *, #2801, .T. ) ;
#19136=CARTESIAN_POINT ( 'NONE',  ( 3.674999999999999822, 0.000000000000000000, 0.000000000000000000 ) ) ;
#19151=CARTESIAN_POINT ( 'NONE',  ( 1.399999999999999911, -13.62500000000000000, -1.668581263838268760E-15 ) ) ;
#19178=CYLINDRICAL_SURFACE ( 'NONE', #8915, 14.59999999999999964 ) ;
#19182=UNCERTAINTY_MEASURE_WITH_UNIT (LENGTH_MEASURE( 1.000000000000000082E-05 ), #20317, 'distance_accuracy_value', 'NONE');
#19187=EDGE_CURVE ( 'NONE', #19843, #296, #16288, .T. ) ;
#19205=CIRCLE ( 'NONE', #5721, 15.25000000000000000 ) ;
#19213=VECTOR ( 'NONE', #5847, 1000.000000000000227 ) ;
#19274=MECHANICAL_DESIGN_GEOMETRIC_PRESENTATION_REPRESENTATION('',(#18274),#12360);
#19280=CARTESIAN_POINT ( 'NONE',  ( 4.025000000000000355, 17.52499999999999858, 0.000000000000000000 ) ) ;
#19289=ORIENTED_EDGE ( 'NONE', *, *, #7753, .F. ) ;
#19290=EDGE_CURVE ( 'NONE', #2774, #8147, #10633, .T. ) ;
#19303=VERTEX_POINT ( 'NONE', #4351 ) ;
#19306=VERTEX_POINT ( 'NONE', #4655 ) ;
#19325=EDGE_CURVE ( 'NONE', #296, #11484, #18857, .T. ) ;
#19326=EDGE_LOOP ( 'NONE', ( #12545, #7169 ) ) ;
#19327=ADVANCED_FACE ( 'NONE', ( #11051 ), #16305, .F. ) ;
#19351=EDGE_CURVE ( 'NONE', #6321, #13610, #15901, .T. ) ;
#19361=FACE_OUTER_BOUND ( 'NONE', #4365, .T. ) ;
#19406=DIRECTION ( 'NONE',  ( -1.000000000000000000, 0.000000000000000000, 0.000000000000000000 ) ) ;
#19407=AXIS2_PLACEMENT_3D ( 'NONE', #12746, #14167, #5008 ) ;
#19427=ORIENTED_EDGE ( 'NONE', *, *, #19351, .F. ) ;
#19448=VERTEX_POINT ( 'NONE', #13215 ) ;
#19458=CARTESIAN_POINT ( 'NONE',  ( -1.776356839400249676E-15, 0.000000000000000000, 0.000000000000000000 ) ) ;
#19464=CARTESIAN_POINT ( 'NONE',  ( 1.050000000000000044, 16.38749999999999929, 0.000000000000000000 ) ) ;
#19478=LINE ( 'NONE', #6851, #17518 ) ;
#19493=ORIENTED_EDGE ( 'NONE', *, *, #9139, .T. ) ;
#19502=EDGE_LOOP ( 'NONE', ( #11171, #15551, #10845, #10738, #4637 ) ) ;
#19589=DIRECTION ( 'NONE',  ( 0.000000000000000000, 1.000000000000000000, 0.000000000000000000 ) ) ;
#19597=ORIENTED_EDGE ( 'NONE', *, *, #6258, .T. ) ;
#19601=FACE_OUTER_BOUND ( 'NONE', #11350, .T. ) ;
#19612=VERTEX_POINT ( 'NONE', #16720 ) ;
#19639=EDGE_LOOP ( 'NONE', ( #3051, #14874, #18818, #3370 ) ) ;
#19649=CARTESIAN_POINT ( 'NONE',  ( 3.674999999999999822, 14.43750000000000000, 0.000000000000000000 ) ) ;
#19669=FACE_OUTER_BOUND ( 'NONE', #18682, .T. ) ;
#19679=VERTEX_POINT ( 'NONE', #12605 ) ;
#19743=UNCERTAINTY_MEASURE_WITH_UNIT (LENGTH_MEASURE( 1.000000000000000082E-05 ), #11620, 'distance_accuracy_value', 'NONE');
#19823=AXIS2_PLACEMENT_3D ( 'NONE', #1263, #18619, #6466 ) ;
#19832=CARTESIAN_POINT ( 'NONE',  ( 5.945602903476760126, 13.89560290347679938, 0.000000000000000000 ) ) ;
#19843=VERTEX_POINT ( 'NONE', #11468 ) ;
#19877=ORIENTED_EDGE ( 'NONE', *, *, #68, .T. ) ;
#19892=FACE_OUTER_BOUND ( 'NONE', #15106, .T. ) ;
#19919=ORIENTED_EDGE ( 'NONE', *, *, #10440, .F. ) ;
#19920=ADVANCED_FACE ( 'NONE', ( #19892 ), #7580, .T. ) ;
#19924=AXIS2_PLACEMENT_3D ( 'NONE', #16921, #7635, #9088 ) ;
#19971=EDGE_CURVE ( 'NONE', #19843, #19448, #1014, .T. ) ;
#19996=ADVANCED_FACE ( 'NONE', ( #17655 ), #7269, .F. ) ;
#20014=ORIENTED_EDGE ( 'NONE', *, *, #9718, .T. ) ;
#20026=FACE_OUTER_BOUND ( 'NONE', #15972, .T. ) ;
#20051=LINE ( 'NONE', #15449, #5740 ) ;
#20063=DIRECTION ( 'NONE',  ( 1.000000000000000000, 0.000000000000000000, 0.000000000000000000 ) ) ;
#20066=AXIS2_PLACEMENT_3D ( 'NONE', #11760, #16503, #14950 ) ;
#20109=DIRECTION ( 'NONE',  ( 1.000000000000000000, 0.000000000000000000, 0.000000000000000000 ) ) ;
#20125=AXIS2_PLACEMENT_3D ( 'NONE', #14560, #11380, #8289 ) ;
#20128=DIRECTION ( 'NONE',  ( 1.000000000000000000, 0.000000000000000000, 0.000000000000000000 ) ) ;
#20138=EDGE_CURVE ( 'NONE', #17493, #10815, #13606, .T. ) ;
#20146=DIRECTION ( 'NONE',  ( 0.000000000000000000, 1.000000000000000000, 0.000000000000000000 ) ) ;
#20232=CARTESIAN_POINT ( 'NONE',  ( 3.324999999999999734, 0.000000000000000000, 0.000000000000000000 ) ) ;
#20246=EDGE_CURVE ( 'NONE', #296, #19843, #1744, .T. ) ;
#20249=ORIENTED_EDGE ( 'NONE', *, *, #6881, .F. ) ;
#20262=AXIS2_PLACEMENT_3D ( 'NONE', #16521, #11670, #4036 ) ;
#20273=ORIENTED_EDGE ( 'NONE', *, *, #10440, .T. ) ;
#20298=DIRECTION ( 'NONE',  ( 0.9999937692730440641, 0.003530072958125829961, 0.000000000000000000 ) ) ;
#20311=ADVANCED_FACE ( 'NONE', ( #6285 ), #15935, .T. ) ;
#20317=( LENGTH_UNIT ( ) NAMED_UNIT ( * ) SI_UNIT ( .MILLI., .METRE. ) );
#20344=CARTESIAN_POINT ( 'NONE',  ( 0.3499999999999999778, 0.000000000000000000, 0.000000000000000000 ) ) ;
#20347=CYLINDRICAL_SURFACE ( 'NONE', #6536, 17.52499999999999858 ) ;
#20362=EDGE_LOOP ( 'NONE', ( #4118, #18734, #12738, #10373 ) ) ;
#20372=DIRECTION ( 'NONE',  ( 0.000000000000000000, 1.000000000000000000, 0.000000000000000000 ) ) ;
ENDSEC;
END-ISO-10303-21;
